ISO-10303-21;
HEADER;
FILE_DESCRIPTION (('STEP AP214'),
    '1' );
FILE_NAME ('needle roller bearing_nh_iso_ISO 3245 - 2521D - 24,SI,NC,24.step',
    '2026-10-08T08:02:49',
    ( '' ),
    ( '' ),
    'SwSTEP 2.0',
    'SolidWorks 2026',
    '' );
FILE_SCHEMA (( 'AUTOMOTIVE_DESIGN' ));
ENDSEC;

DATA;
#9=ORIENTED_EDGE ( 'NONE', *, *, #20619, .T. ) ;
#72=DIRECTION ( 'NONE',  ( -1.000000000000000000, 0.000000000000000000, -0.000000000000000000 ) ) ;
#128=EDGE_CURVE ( 'NONE', #41039, #1919, #35074, .T. ) ;
#145=AXIS2_PLACEMENT_3D ( 'NONE', #52152, #34003, #4829 ) ;
#194=AXIS2_PLACEMENT_3D ( 'NONE', #25352, #281, #58847 ) ;
#264=( NAMED_UNIT ( * ) PLANE_ANGLE_UNIT ( ) SI_UNIT ( $, .RADIAN. ) );
#281=DIRECTION ( 'NONE',  ( -1.000000000000000000, -0.000000000000000000, -0.000000000000000000 ) ) ;
#367=CARTESIAN_POINT ( 'NONE',  ( 5.331199999999999939, 0.000000000000000000, 12.55882000000000076 ) ) ;
#536=VERTEX_POINT ( 'NONE', #46883 ) ;
#679=CARTESIAN_POINT ( 'NONE',  ( 5.999999999999998224, 6.934333478519240412E-15, 0.000000000000000000 ) ) ;
#691=ORIENTED_EDGE ( 'NONE', *, *, #39031, .F. ) ;
#703=CIRCLE ( 'NONE', #14728, 15.38217999999999996 ) ;
#792=CARTESIAN_POINT ( 'NONE',  ( 5.283180000000047727, 0.000000000000000000, 15.43999999999999240 ) ) ;
#825=DIRECTION ( 'NONE',  ( -1.655270492344282294E-16, 1.000000000000000000, 0.000000000000000000 ) ) ;
#921=ADVANCED_FACE ( 'NONE', ( #33014, #18595 ), #48023, .F. ) ;
#959=ORIENTED_EDGE ( 'NONE', *, *, #22632, .F. ) ;
#967=DIRECTION ( 'NONE',  ( 1.000000000000000000, 1.836909530733573776E-16, 0.000000000000000000 ) ) ;
#1029=VERTEX_POINT ( 'NONE', #34856 ) ;
#1233=CARTESIAN_POINT ( 'NONE',  ( -6.000000000000001776, 4.730042041638951881E-15, 0.000000000000000000 ) ) ;
#1396=DIRECTION ( 'NONE',  ( 1.000000000000000000, 1.836909530733573776E-16, 0.000000000000000000 ) ) ;
#1430=DIRECTION ( 'NONE',  ( 0.000000000000000000, 0.000000000000000000, -1.000000000000000000 ) ) ;
#1476=VERTEX_POINT ( 'NONE', #3264 ) ;
#1749=VERTEX_POINT ( 'NONE', #51119 ) ;
#1752=CARTESIAN_POINT ( 'NONE',  ( 5.440000000000000391, 6.831466544798160849E-15, 0.000000000000000000 ) ) ;
#1863=ORIENTED_EDGE ( 'NONE', *, *, #30854, .T. ) ;
#1919=VERTEX_POINT ( 'NONE', #59766 ) ;
#2069=AXIS2_PLACEMENT_3D ( 'NONE', #36760, #8523, #46159 ) ;
#2078=CARTESIAN_POINT ( 'NONE',  ( -5.283180000000052168, 0.000000000000000000, 15.43999999999999240 ) ) ;
#2080=ADVANCED_FACE ( 'NONE', ( #4580 ), #61294, .F. ) ;
#2212=DIRECTION ( 'NONE',  ( -1.000000000000000000, -0.000000000000000000, -0.000000000000000000 ) ) ;
#2219=ORIENTED_EDGE ( 'NONE', *, *, #2595, .F. ) ;
#2243=FACE_OUTER_BOUND ( 'NONE', #31690, .T. ) ;
#2260=CARTESIAN_POINT ( 'NONE',  ( -31.75000000000000000, 0.000000000000000000, 0.000000000000000000 ) ) ;
#2328=CARTESIAN_POINT ( 'NONE',  ( -31.75000000000000000, -15.14599999999999369, 1.854850041988580438E-15 ) ) ;
#2354=AXIS2_PLACEMENT_3D ( 'NONE', #34177, #30686, #30071 ) ;
#2478=VERTEX_POINT ( 'NONE', #57430 ) ;
#2580=CIRCLE ( 'NONE', #7582, 15.14599999999999369 ) ;
#2585=AXIS2_PLACEMENT_3D ( 'NONE', #44389, #54037, #49354 ) ;
#2595=EDGE_CURVE ( 'NONE', #5803, #59492, #29106, .T. ) ;
#2615=CARTESIAN_POINT ( 'NONE',  ( -31.75000000000000000, 15.43999999999999240, 0.000000000000000000 ) ) ;
#2654=CIRCLE ( 'NONE', #53704, 0.05882000000000109363 ) ;
#2800=ORIENTED_EDGE ( 'NONE', *, *, #15957, .F. ) ;
#2905=EDGE_CURVE ( 'NONE', #61046, #46997, #36148, .T. ) ;
#2971=DIRECTION ( 'NONE',  ( -1.000000000000000000, -0.000000000000000000, -0.000000000000000000 ) ) ;
#3080=ORIENTED_EDGE ( 'NONE', *, *, #61543, .T. ) ;
#3085=EDGE_LOOP ( 'NONE', ( #44814, #33317 ) ) ;
#3167=ORIENTED_EDGE ( 'NONE', *, *, #48873, .T. ) ;
#3264=CARTESIAN_POINT ( 'NONE',  ( -5.439999999999997726, -15.43999999999999062, 1.890854657883512912E-15 ) ) ;
#3415=CARTESIAN_POINT ( 'NONE',  ( -31.75000000000000000, -15.43999999999999240, 1.890854657883512518E-15 ) ) ;
#3420=AXIS2_PLACEMENT_3D ( 'NONE', #43752, #41976, #38424 ) ;
#3535=ORIENTED_EDGE ( 'NONE', *, *, #39693, .T. ) ;
#3593=TOROIDAL_SURFACE ( 'NONE', #38647, 15.71999999999999709, 0.2800000000000011924 ) ;
#3732=CARTESIAN_POINT ( 'NONE',  ( -5.283180000000052168, -15.43999999999999417, 1.890854657883513307E-15 ) ) ;
#3759=CARTESIAN_POINT ( 'NONE',  ( 0.000000000000000000, 0.000000000000000000, 0.000000000000000000 ) ) ;
#3776=ORIENTED_EDGE ( 'NONE', *, *, #15510, .F. ) ;
#3794=VERTEX_POINT ( 'NONE', #11645 ) ;
#3947=ORIENTED_EDGE ( 'NONE', *, *, #51571, .T. ) ;
#3973=DIRECTION ( 'NONE',  ( 1.000000000000000000, 1.836909530733573776E-16, 0.000000000000000000 ) ) ;
#3994=CLOSED_SHELL ( 'NONE', ( #54130, #16326, #21800, #32420, #60555, #17854, #48300, #19035, #47503, #31319, #8760, #13309, #37233, #21166, #10050, #57395, #49127, #61148, #35906, #49288, #10186, #2080, #58713, #14983, #52657, #35997, #921, #30125, #26803, #27121 ) ) ;
#4044=FACE_OUTER_BOUND ( 'NONE', #21656, .T. ) ;
#4136=DIRECTION ( 'NONE',  ( -1.000000000000000000, -0.000000000000000000, -0.000000000000000000 ) ) ;
#4172=VECTOR ( 'NONE', #48172, 1000.000000000000000 ) ;
#4289=EDGE_CURVE ( 'NONE', #19981, #2478, #46959, .T. ) ;
#4304=ORIENTED_EDGE ( 'NONE', *, *, #28194, .F. ) ;
#4325=ORIENTED_EDGE ( 'NONE', *, *, #21791, .F. ) ;
#4434=CARTESIAN_POINT ( 'NONE',  ( 5.283180000000047727, 0.000000000000000000, 0.000000000000000000 ) ) ;
#4439=ORIENTED_EDGE ( 'NONE', *, *, #21791, .T. ) ;
#4580=FACE_OUTER_BOUND ( 'NONE', #55032, .T. ) ;
#4584=DIRECTION ( 'NONE',  ( 1.000000000000000000, 1.836909530733573776E-16, 0.000000000000000000 ) ) ;
#4610=CARTESIAN_POINT ( 'NONE',  ( 5.999999999999998224, 6.934333478519240412E-15, 0.000000000000000000 ) ) ;
#4712=ORIENTED_EDGE ( 'NONE', *, *, #60431, .T. ) ;
#4736=AXIS2_PLACEMENT_3D ( 'NONE', #11626, #967, #54189 ) ;
#4743=DIRECTION ( 'NONE',  ( -1.718001593797181987E-16, 1.000000000000000000, 0.000000000000000000 ) ) ;
#4761=EDGE_CURVE ( 'NONE', #59492, #5803, #11956, .T. ) ;
#4802=CARTESIAN_POINT ( 'NONE',  ( -31.75000000000000000, 0.000000000000000000, 0.000000000000000000 ) ) ;
#4810=PLANE ( 'NONE',  #34838 ) ;
#4829=DIRECTION ( 'NONE',  ( 0.000000000000000000, -1.000000000000000000, 1.224646799147349509E-16 ) ) ;
#4974=AXIS2_PLACEMENT_3D ( 'NONE', #49408, #20908, #58787 ) ;
#4975=CARTESIAN_POINT ( 'NONE',  ( 5.272379999999998290, 0.000000000000000000, 0.000000000000000000 ) ) ;
#4994=VERTEX_POINT ( 'NONE', #9394 ) ;
#5161=ORIENTED_EDGE ( 'NONE', *, *, #37834, .F. ) ;
#5183=ORIENTED_EDGE ( 'NONE', *, *, #16154, .F. ) ;
#5190=ORIENTED_EDGE ( 'NONE', *, *, #2905, .F. ) ;
#5239=DIRECTION ( 'NONE',  ( -1.655270492344282294E-16, 1.000000000000000000, 0.000000000000000000 ) ) ;
#5342=AXIS2_PLACEMENT_3D ( 'NONE', #26762, #36183, #20836 ) ;
#5474=VECTOR ( 'NONE', #55797, 1000.000000000000000 ) ;
#5504=CARTESIAN_POINT ( 'NONE',  ( 5.999999999999998224, 6.934333478519240412E-15, 0.000000000000000000 ) ) ;
#5532=CARTESIAN_POINT ( 'NONE',  ( 5.999999999999995559, 15.72000000000000064, 0.000000000000000000 ) ) ;
#5641=VERTEX_POINT ( 'NONE', #367 ) ;
#5803=VERTEX_POINT ( 'NONE', #32616 ) ;
#5820=CIRCLE ( 'NONE', #25831, 15.99999999999999645 ) ;
#6196=FACE_OUTER_BOUND ( 'NONE', #10720, .T. ) ;
#6254=AXIS2_PLACEMENT_3D ( 'NONE', #32974, #28550, #42678 ) ;
#6317=CARTESIAN_POINT ( 'NONE',  ( -31.75000000000000000, 0.000000000000000000, 0.000000000000000000 ) ) ;
#6398=DIRECTION ( 'NONE',  ( 0.000000000000000000, 0.000000000000000000, -1.000000000000000000 ) ) ;
#6414=DIRECTION ( 'NONE',  ( 1.000000000000000000, 1.836909530733573776E-16, 0.000000000000000000 ) ) ;
#6438=DIRECTION ( 'NONE',  ( 0.000000000000000000, 0.000000000000000000, 1.000000000000000000 ) ) ;
#6461=ORIENTED_EDGE ( 'NONE', *, *, #22632, .T. ) ;
#6493=VECTOR ( 'NONE', #1396, 1000.000000000000000 ) ;
#6509=FACE_OUTER_BOUND ( 'NONE', #7401, .T. ) ;
#6540=EDGE_CURVE ( 'NONE', #4994, #55598, #8321, .T. ) ;
#6598=ORIENTED_EDGE ( 'NONE', *, *, #13975, .F. ) ;
#6717=FACE_OUTER_BOUND ( 'NONE', #36250, .T. ) ;
#6742=DIRECTION ( 'NONE',  ( 0.000000000000000000, 1.000000000000000000, 0.000000000000000000 ) ) ;
#6769=FACE_OUTER_BOUND ( 'NONE', #30520, .T. ) ;
#6803=CARTESIAN_POINT ( 'NONE',  ( 5.719999999999999751, -15.71999999999998820, 1.925144768259638627E-15 ) ) ;
#6894=CARTESIAN_POINT ( 'NONE',  ( -6.000000000000003553, 15.14599999999999902, 0.000000000000000000 ) ) ;
#6955=FACE_OUTER_BOUND ( 'NONE', #18450, .T. ) ;
#6971=DIRECTION ( 'NONE',  ( -1.000000000000000000, -0.000000000000000000, -0.000000000000000000 ) ) ;
#7296=AXIS2_PLACEMENT_3D ( 'NONE', #30275, #45335, #6438 ) ;
#7298=ORIENTED_EDGE ( 'NONE', *, *, #25716, .T. ) ;
#7338=COLOUR_RGB ( '', 0.31764706, 0.68627451, 0.89019608) ;
#7401=EDGE_LOOP ( 'NONE', ( #58328, #35295, #21517, #50860 ) ) ;
#7582=AXIS2_PLACEMENT_3D ( 'NONE', #48912, #19807, #20412 ) ;
#7622=CIRCLE ( 'NONE', #56637, 15.43999999999999240 ) ;
#7719=ORIENTED_EDGE ( 'NONE', *, *, #40009, .F. ) ;
#7726=ORIENTED_EDGE ( 'NONE', *, *, #30854, .F. ) ;
#7806=AXIS2_PLACEMENT_3D ( 'NONE', #47297, #37610, #51672 ) ;
#7827=CYLINDRICAL_SURFACE ( 'NONE', #56360, 12.49999999999999822 ) ;
#7885=CARTESIAN_POINT ( 'NONE',  ( -31.75000000000000000, 0.000000000000000000, 0.000000000000000000 ) ) ;
#8189=CYLINDRICAL_SURFACE ( 'NONE', #25650, 16.00000000000000000 ) ;
#8201=ORIENTED_EDGE ( 'NONE', *, *, #31758, .F. ) ;
#8212=DIRECTION ( 'NONE',  ( 0.000000000000000000, 0.000000000000000000, 1.000000000000000000 ) ) ;
#8263=CIRCLE ( 'NONE', #60308, 15.43999999999999240 ) ;
#8321=LINE ( 'NONE', #16832, #8839 ) ;
#8340=CARTESIAN_POINT ( 'NONE',  ( 5.440000000000000391, 6.831466544798160849E-15, 0.000000000000000000 ) ) ;
#8358=FACE_OUTER_BOUND ( 'NONE', #52722, .T. ) ;
#8477=AXIS2_PLACEMENT_3D ( 'NONE', #20224, #48713, #15831 ) ;
#8489=CARTESIAN_POINT ( 'NONE',  ( 5.331200000000000827, 1.887314203987178256E-15, -15.38217999999999996 ) ) ;
#8523=DIRECTION ( 'NONE',  ( 1.000000000000000000, 1.836909530733573776E-16, 0.000000000000000000 ) ) ;
#8533=EDGE_LOOP ( 'NONE', ( #56396, #12459 ) ) ;
#8663=PLANE ( 'NONE',  #21844 ) ;
#8733=LINE ( 'NONE', #42898, #13653 ) ;
#8760=ADVANCED_FACE ( 'NONE', ( #51331 ), #19307, .F. ) ;
#8791=VERTEX_POINT ( 'NONE', #20234 ) ;
#8835=FACE_BOUND ( 'NONE', #30751, .T. ) ;
#8839=VECTOR ( 'NONE', #12141, 1000.000000000000000 ) ;
#9002=CARTESIAN_POINT ( 'NONE',  ( 5.440000000000000391, 6.831466544798160849E-15, 0.000000000000000000 ) ) ;
#9038=ORIENTED_EDGE ( 'NONE', *, *, #46850, .F. ) ;
#9137=DIRECTION ( 'NONE',  ( 1.000000000000000000, 1.836909530733573776E-16, 0.000000000000000000 ) ) ;
#9143=DIRECTION ( 'NONE',  ( -1.000000000000000000, -0.000000000000000000, -0.000000000000000000 ) ) ;
#9327=CARTESIAN_POINT ( 'NONE',  ( 5.999999999999995559, 15.14599999999999902, 0.000000000000000000 ) ) ;
#9373=( NAMED_UNIT ( * ) PLANE_ANGLE_UNIT ( ) SI_UNIT ( $, .RADIAN. ) );
#9394=CARTESIAN_POINT ( 'NONE',  ( -6.000000000000004441, 15.14599999999999902, 0.000000000000000000 ) ) ;
#9521=FACE_OUTER_BOUND ( 'NONE', #45722, .T. ) ;
#9738=DIRECTION ( 'NONE',  ( -1.000000000000000000, -0.000000000000000000, -0.000000000000000000 ) ) ;
#9778=AXIS2_PLACEMENT_3D ( 'NONE', #51653, #51965, #61961 ) ;
#9839=SURFACE_STYLE_FILL_AREA ( #34821 ) ;
#9847=CIRCLE ( 'NONE', #25848, 15.38218000000000174 ) ;
#10050=ADVANCED_FACE ( 'NONE', ( #13393, #51569 ), #8663, .T. ) ;
#10098=DIRECTION ( 'NONE',  ( -1.000000000000000000, -0.000000000000000000, -0.000000000000000000 ) ) ;
#10157=FACE_BOUND ( 'NONE', #19069, .T. ) ;
#10186=ADVANCED_FACE ( 'NONE', ( #6717, #8835 ), #32044, .T. ) ;
#10192=CIRCLE ( 'NONE', #194, 12.55882000000000076 ) ;
#10315=( LENGTH_UNIT ( ) NAMED_UNIT ( * ) SI_UNIT ( .MILLI., .METRE. ) );
#10518=LINE ( 'NONE', #2328, #6493 ) ;
#10596=ORIENTED_EDGE ( 'NONE', *, *, #53503, .T. ) ;
#10720=EDGE_LOOP ( 'NONE', ( #39977, #38541, #61337, #42509, #15156 ) ) ;
#10831=SHAPE_REPRESENTATION ( 'needle roller bearing_nh_iso_ISO 3245 - 2521D - 24,SI,NC,24', ( #14677 ), #31864 ) ;
#10862=EDGE_CURVE ( 'NONE', #1919, #25747, #46913, .T. ) ;
#10909=CARTESIAN_POINT ( 'NONE',  ( -5.331200000000000827, 0.000000000000000000, 12.55882000000000076 ) ) ;
#11010=( NAMED_UNIT ( * ) SI_UNIT ( $, .STERADIAN. ) SOLID_ANGLE_UNIT ( ) );
#11127=ORIENTED_EDGE ( 'NONE', *, *, #23636, .F. ) ;
#11224=TOROIDAL_SURFACE ( 'NONE', #17217, 15.38217999999999996, 0.05882000000000066342 ) ;
#11235=VERTEX_POINT ( 'NONE', #54667 ) ;
#11310=AXIS2_PLACEMENT_3D ( 'NONE', #46254, #52157, #50921 ) ;
#11319=DIRECTION ( 'NONE',  ( 1.000000000000000000, 1.836909530733573776E-16, 0.000000000000000000 ) ) ;
#11324=DIRECTION ( 'NONE',  ( -1.718001593797181987E-16, 1.000000000000000000, 0.000000000000000000 ) ) ;
#11380=CARTESIAN_POINT ( 'NONE',  ( -5.720000000000002416, 15.72000000000000064, 0.000000000000000000 ) ) ;
#11454=AXIS2_PLACEMENT_3D ( 'NONE', #1233, #39492, #50101 ) ;
#11626=CARTESIAN_POINT ( 'NONE',  ( 5.719999999999997087, 6.938893903907228378E-15, 0.000000000000000000 ) ) ;
#11645=CARTESIAN_POINT ( 'NONE',  ( 5.719999999999993534, 16.00000000000000355, 0.000000000000000000 ) ) ;
#11756=DIRECTION ( 'NONE',  ( 1.000000000000000000, 1.836909530733573776E-16, 0.000000000000000000 ) ) ;
#11776=EDGE_CURVE ( 'NONE', #61479, #5641, #11798, .T. ) ;
#11798=CIRCLE ( 'NONE', #46816, 12.55882000000000076 ) ;
#11810=DIRECTION ( 'NONE',  ( -1.685288351013738396E-16, 1.000000000000000000, 0.000000000000000000 ) ) ;
#11956=CIRCLE ( 'NONE', #42982, 15.14599999999999369 ) ;
#12001=CIRCLE ( 'NONE', #56990, 0.05882000000000109363 ) ;
#12044=EDGE_LOOP ( 'NONE', ( #23332, #38944, #2800, #41973 ) ) ;
#12141=DIRECTION ( 'NONE',  ( 1.000000000000000000, 1.836909530733573776E-16, 0.000000000000000000 ) ) ;
#12232=CARTESIAN_POINT ( 'NONE',  ( -31.75000000000000000, -15.43999999999999240, 1.890854657883512518E-15 ) ) ;
#12321=AXIS2_PLACEMENT_3D ( 'NONE', #38939, #10098, #25416 ) ;
#12419=CARTESIAN_POINT ( 'NONE',  ( 5.272379999999998290, 1.538011871406776419E-15, -12.55882000000000076 ) ) ;
#12459=ORIENTED_EDGE ( 'NONE', *, *, #51327, .T. ) ;
#12475=DIRECTION ( 'NONE',  ( 0.000000000000000000, -1.000000000000000000, 1.224646799147349509E-16 ) ) ;
#12665=AXIS2_PLACEMENT_3D ( 'NONE', #51720, #9738, #48272 ) ;
#12774=DIRECTION ( 'NONE',  ( 1.000000000000000000, 1.836909530733573776E-16, 0.000000000000000000 ) ) ;
#12843=ORIENTED_EDGE ( 'NONE', *, *, #60431, .F. ) ;
#12908=EDGE_LOOP ( 'NONE', ( #39960, #12932, #18583, #41105 ) ) ;
#12914=EDGE_CURVE ( 'NONE', #1029, #35847, #703, .T. ) ;
#12932=ORIENTED_EDGE ( 'NONE', *, *, #27087, .T. ) ;
#12976=UNCERTAINTY_MEASURE_WITH_UNIT (LENGTH_MEASURE( 1.000000000000000082E-05 ), #29104, 'distance_accuracy_value', 'NONE');
#13176=ORIENTED_EDGE ( 'NONE', *, *, #51332, .F. ) ;
#13274=CARTESIAN_POINT ( 'NONE',  ( 5.439999999999996838, 15.14599999999999902, 0.000000000000000000 ) ) ;
#13309=ADVANCED_FACE ( 'NONE', ( #15857 ), #34975, .F. ) ;
#13393=FACE_OUTER_BOUND ( 'NONE', #8533, .T. ) ;
#13653=VECTOR ( 'NONE', #57247, 1000.000000000000000 ) ;
#13688=VERTEX_POINT ( 'NONE', #36999 ) ;
#13718=CARTESIAN_POINT ( 'NONE',  ( -31.75000000000000000, 0.000000000000000000, 0.000000000000000000 ) ) ;
#13791=AXIS2_PLACEMENT_3D ( 'NONE', #44077, #48734, #6398 ) ;
#13806=AXIS2_PLACEMENT_3D ( 'NONE', #4802, #18634, #18020 ) ;
#13822=DIRECTION ( 'NONE',  ( 1.000000000000000000, 0.000000000000000000, 0.000000000000000000 ) ) ;
#13904=AXIS2_PLACEMENT_3D ( 'NONE', #30027, #44475, #20637 ) ;
#13970=ORIENTED_EDGE ( 'NONE', *, *, #20055, .T. ) ;
#13975=EDGE_CURVE ( 'NONE', #46997, #61046, #22637, .T. ) ;
#14105=SURFACE_STYLE_USAGE ( .BOTH. , #52279 ) ;
#14107=AXIS2_PLACEMENT_3D ( 'NONE', #51460, #72, #38331 ) ;
#14233=AXIS2_PLACEMENT_3D ( 'NONE', #28059, #51850, #41252 ) ;
#14238=CARTESIAN_POINT ( 'NONE',  ( 5.283180000000047727, -15.43999999999999240, 1.890854657883513307E-15 ) ) ;
#14297=CARTESIAN_POINT ( 'NONE',  ( -5.272380000000000067, 1.538011871406776419E-15, -12.55882000000000076 ) ) ;
#14357=MECHANICAL_DESIGN_GEOMETRIC_PRESENTATION_REPRESENTATION('',(#40395),#35380);
#14456=ORIENTED_EDGE ( 'NONE', *, *, #37789, .F. ) ;
#14508=PLANE ( 'NONE',  #43569 ) ;
#14677=AXIS2_PLACEMENT_3D ( 'NONE', #3759, #61387, #13822 ) ;
#14728=AXIS2_PLACEMENT_3D ( 'NONE', #17578, #2212, #31055 ) ;
#14983=ADVANCED_FACE ( 'NONE', ( #44791 ), #49677, .T. ) ;
#15132=ORIENTED_EDGE ( 'NONE', *, *, #23090, .F. ) ;
#15156=ORIENTED_EDGE ( 'NONE', *, *, #20619, .F. ) ;
#15157=ORIENTED_EDGE ( 'NONE', *, *, #17284, .T. ) ;
#15333=FILL_AREA_STYLE_COLOUR ( '', #44897 ) ;
#15401=FACE_OUTER_BOUND ( 'NONE', #12908, .T. ) ;
#15503=AXIS2_PLACEMENT_3D ( 'NONE', #49595, #40246, #55523 ) ;
#15510=EDGE_CURVE ( 'NONE', #41881, #46997, #22186, .T. ) ;
#15530=CARTESIAN_POINT ( 'NONE',  ( 5.272380000000000067, 1.530808498934191324E-15, -12.49999999999999822 ) ) ;
#15684=ORIENTED_EDGE ( 'NONE', *, *, #31973, .F. ) ;
#15769=DIRECTION ( 'NONE',  ( 1.000000000000000000, 1.836909530733573776E-16, 0.000000000000000000 ) ) ;
#15831=DIRECTION ( 'NONE',  ( 0.000000000000000000, 0.000000000000000000, 1.000000000000000000 ) ) ;
#15857=FACE_OUTER_BOUND ( 'NONE', #26156, .T. ) ;
#15889=EDGE_LOOP ( 'NONE', ( #34404, #8201, #20581, #54995, #25224 ) ) ;
#15953=CARTESIAN_POINT ( 'NONE',  ( -5.999999999999999112, -15.14599999999999014, 1.854850041988580438E-15 ) ) ;
#15957=EDGE_CURVE ( 'NONE', #5641, #61479, #10192, .T. ) ;
#16005=VERTEX_POINT ( 'NONE', #54138 ) ;
#16042=PRODUCT_DEFINITION_CONTEXT ( 'detailed design', #34463, 'design' ) ;
#16046=ORIENTED_EDGE ( 'NONE', *, *, #4289, .F. ) ;
#16154=EDGE_CURVE ( 'NONE', #35697, #1749, #49086, .T. ) ;
#16179=DIRECTION ( 'NONE',  ( 0.000000000000000000, -1.000000000000000000, 0.000000000000000000 ) ) ;
#16255=PRODUCT ( 'needle roller bearing_nh_iso_ISO 3245 - 2521D - 24,SI,NC,24', 'needle roller bearing_nh_iso_ISO 3245 - 2521D - 24,SI,NC,24', '', ( #17404 ) ) ;
#16261=DIRECTION ( 'NONE',  ( 1.000000000000000000, 1.836909530733573776E-16, 0.000000000000000000 ) ) ;
#16288=TOROIDAL_SURFACE ( 'NONE', #12321, 12.55882000000000076, 0.05882000000000109363 ) ;
#16326=ADVANCED_FACE ( 'NONE', ( #31841 ), #40270, .T. ) ;
#16450=DIRECTION ( 'NONE',  ( 0.000000000000000000, 0.000000000000000000, 1.000000000000000000 ) ) ;
#16558=CARTESIAN_POINT ( 'NONE',  ( 5.439999999999997726, 15.43999999999999950, 0.000000000000000000 ) ) ;
#16602=EDGE_CURVE ( 'NONE', #35847, #1029, #46250, .T. ) ;
#16789=DIRECTION ( 'NONE',  ( 0.000000000000000000, 0.000000000000000000, 1.000000000000000000 ) ) ;
#16832=CARTESIAN_POINT ( 'NONE',  ( -31.75000000000000000, 15.14599999999999369, 0.000000000000000000 ) ) ;
#16846=MECHANICAL_DESIGN_GEOMETRIC_PRESENTATION_REPRESENTATION('',(#59841),#27828);
#16867=DIRECTION ( 'NONE',  ( 0.000000000000000000, -1.224646799147332007E-16, 1.000000000000000000 ) ) ;
#16973=CIRCLE ( 'NONE', #46045, 12.49999999999999822 ) ;
#17073=EDGE_LOOP ( 'NONE', ( #61687, #20984, #5190, #55660 ) ) ;
#17217=AXIS2_PLACEMENT_3D ( 'NONE', #4975, #30034, #28803 ) ;
#17228=LINE ( 'NONE', #12232, #36277 ) ;
#17284=EDGE_CURVE ( 'NONE', #40440, #2478, #17228, .T. ) ;
#17404=PRODUCT_CONTEXT ( 'NONE', #26741, 'mechanical' ) ;
#17578=CARTESIAN_POINT ( 'NONE',  ( 5.331200000000000827, 0.000000000000000000, 0.000000000000000000 ) ) ;
#17779=CARTESIAN_POINT ( 'NONE',  ( -6.000000000000004441, 15.72000000000000064, 0.000000000000000000 ) ) ;
#17805=PRODUCT_DEFINITION_SHAPE ( 'NONE', 'NONE',  #51660 ) ;
#17854=ADVANCED_FACE ( 'NONE', ( #44293 ), #54250, .F. ) ;
#18020=DIRECTION ( 'NONE',  ( 0.000000000000000000, 1.000000000000000000, 0.000000000000000000 ) ) ;
#18172=DIRECTION ( 'NONE',  ( 0.000000000000000000, 0.000000000000000000, 1.000000000000000000 ) ) ;
#18397=DIRECTION ( 'NONE',  ( -1.836909530733573776E-16, 1.000000000000000000, 0.000000000000000000 ) ) ;
#18419=ORIENTED_EDGE ( 'NONE', *, *, #51327, .F. ) ;
#18450=EDGE_LOOP ( 'NONE', ( #20386, #43809, #55922, #6461, #36152 ) ) ;
#18475=CIRCLE ( 'NONE', #36507, 15.71999999999999709 ) ;
#18541=EDGE_CURVE ( 'NONE', #35847, #16005, #33794, .T. ) ;
#18583=ORIENTED_EDGE ( 'NONE', *, *, #48873, .F. ) ;
#18595=FACE_BOUND ( 'NONE', #26023, .T. ) ;
#18605=VERTEX_POINT ( 'NONE', #59752 ) ;
#18634=DIRECTION ( 'NONE',  ( 1.000000000000000000, 1.836909530733573776E-16, 0.000000000000000000 ) ) ;
#18654=AXIS2_PLACEMENT_3D ( 'NONE', #37182, #60954, #45970 ) ;
#18728=DIRECTION ( 'NONE',  ( -1.626303258728256898E-16, 1.000000000000000000, 0.000000000000000000 ) ) ;
#18798=SURFACE_STYLE_FILL_AREA ( #38226 ) ;
#19035=ADVANCED_FACE ( 'NONE', ( #9521 ), #47443, .T. ) ;
#19069=EDGE_LOOP ( 'NONE', ( #54363, #10596 ) ) ;
#19307=CYLINDRICAL_SURFACE ( 'NONE', #3420, 15.43999999999999240 ) ;
#19559=PRESENTATION_STYLE_ASSIGNMENT (( #23025 ) ) ;
#19657=ORIENTED_EDGE ( 'NONE', *, *, #20252, .F. ) ;
#19807=DIRECTION ( 'NONE',  ( 1.000000000000000000, 1.836909530733573776E-16, 0.000000000000000000 ) ) ;
#19943=ORIENTED_EDGE ( 'NONE', *, *, #16602, .F. ) ;
#19981=VERTEX_POINT ( 'NONE', #16558 ) ;
#20055=EDGE_CURVE ( 'NONE', #61884, #42948, #45733, .T. ) ;
#20146=EDGE_LOOP ( 'NONE', ( #5183, #34473, #44969, #59811 ) ) ;
#20224=CARTESIAN_POINT ( 'NONE',  ( -5.272380000000000067, 0.000000000000000000, 0.000000000000000000 ) ) ;
#20234=CARTESIAN_POINT ( 'NONE',  ( -5.440000000000003055, 15.43999999999999950, 0.000000000000000000 ) ) ;
#20252=EDGE_CURVE ( 'NONE', #38956, #25747, #38497, .T. ) ;
#20386=ORIENTED_EDGE ( 'NONE', *, *, #17284, .F. ) ;
#20412=DIRECTION ( 'NONE',  ( -1.718001593797181987E-16, 1.000000000000000000, 0.000000000000000000 ) ) ;
#20448=CARTESIAN_POINT ( 'NONE',  ( -5.720000000000000639, 3.469446951953614189E-15, 0.000000000000000000 ) ) ;
#20452=CARTESIAN_POINT ( 'NONE',  ( -5.440000000000000391, 4.832908975360033023E-15, 0.000000000000000000 ) ) ;
#20579=EDGE_CURVE ( 'NONE', #40440, #39188, #21480, .T. ) ;
#20581=ORIENTED_EDGE ( 'NONE', *, *, #45221, .F. ) ;
#20606=ORIENTED_EDGE ( 'NONE', *, *, #60165, .T. ) ;
#20619=EDGE_CURVE ( 'NONE', #16005, #40440, #34509, .T. ) ;
#20637=DIRECTION ( 'NONE',  ( 0.000000000000000000, 0.000000000000000000, 1.000000000000000000 ) ) ;
#20644=CARTESIAN_POINT ( 'NONE',  ( 5.331200000000000827, 0.000000000000000000, 0.000000000000000000 ) ) ;
#20704=CIRCLE ( 'NONE', #26683, 15.43999999999999240 ) ;
#20805=AXIS2_PLACEMENT_3D ( 'NONE', #61285, #36285, #42529 ) ;
#20836=DIRECTION ( 'NONE',  ( -1.626303258728256898E-16, 1.000000000000000000, 0.000000000000000000 ) ) ;
#20846=DIRECTION ( 'NONE',  ( 0.000000000000000000, 0.000000000000000000, 1.000000000000000000 ) ) ;
#20908=DIRECTION ( 'NONE',  ( -1.000000000000000000, -0.000000000000000000, -0.000000000000000000 ) ) ;
#20984=ORIENTED_EDGE ( 'NONE', *, *, #15510, .T. ) ;
#21166=ADVANCED_FACE ( 'NONE', ( #39395 ), #49686, .F. ) ;
#21212=DIRECTION ( 'NONE',  ( -1.685288351013738149E-16, 1.000000000000000000, 0.000000000000000000 ) ) ;
#21395=EDGE_CURVE ( 'NONE', #35697, #61479, #22517, .T. ) ;
#21480=CIRCLE ( 'NONE', #15503, 15.43999999999999240 ) ;
#21517=ORIENTED_EDGE ( 'NONE', *, *, #46850, .T. ) ;
#21560=AXIS2_PLACEMENT_3D ( 'NONE', #11380, #58653, #54569 ) ;
#21603=ORIENTED_EDGE ( 'NONE', *, *, #25716, .F. ) ;
#21612=CARTESIAN_POINT ( 'NONE',  ( -5.283180000000052168, 0.000000000000000000, 0.000000000000000000 ) ) ;
#21656=EDGE_LOOP ( 'NONE', ( #38390, #39844, #20606, #12843 ) ) ;
#21677=VECTOR ( 'NONE', #47341, 1000.000000000000000 ) ;
#21791=EDGE_CURVE ( 'NONE', #27783, #16005, #8263, .T. ) ;
#21800=ADVANCED_FACE ( 'NONE', ( #43018 ), #16288, .T. ) ;
#21844=AXIS2_PLACEMENT_3D ( 'NONE', #61279, #33120, #18397 ) ;
#22186=CIRCLE ( 'NONE', #145, 0.2800000000000024691 ) ;
#22283=CARTESIAN_POINT ( 'NONE',  ( -5.272380000000000067, 1.883773750090843600E-15, -15.38217999999999996 ) ) ;
#22306=DIRECTION ( 'NONE',  ( 0.000000000000000000, 1.000000000000000000, 0.000000000000000000 ) ) ;
#22327=CARTESIAN_POINT ( 'NONE',  ( 5.331200000000000827, 0.000000000000000000, 0.000000000000000000 ) ) ;
#22328=CARTESIAN_POINT ( 'NONE',  ( 5.283180000000047727, 15.43999999999999240, 0.000000000000000000 ) ) ;
#22517=CIRCLE ( 'NONE', #44547, 0.05882000000000109363 ) ;
#22547=CARTESIAN_POINT ( 'NONE',  ( -5.331200000000000827, 0.000000000000000000, 15.38218000000000174 ) ) ;
#22610=CARTESIAN_POINT ( 'NONE',  ( -25.39999999999999858, 0.000000000000000000, 12.49999999999999822 ) ) ;
#22629=FACE_OUTER_BOUND ( 'NONE', #15889, .T. ) ;
#22632=EDGE_CURVE ( 'NONE', #27783, #19981, #50854, .T. ) ;
#22637=CIRCLE ( 'NONE', #44650, 16.00000000000000000 ) ;
#22681=ORIENTED_EDGE ( 'NONE', *, *, #45155, .T. ) ;
#22844=CIRCLE ( 'NONE', #61804, 15.71999999999999353 ) ;
#22973=EDGE_LOOP ( 'NONE', ( #11127, #23838, #33345, #30199 ) ) ;
#23025=SURFACE_STYLE_USAGE ( .BOTH. , #48059 ) ;
#23064=EDGE_CURVE ( 'NONE', #1029, #39188, #38001, .T. ) ;
#23090=EDGE_CURVE ( 'NONE', #1476, #48507, #51037, .T. ) ;
#23332=ORIENTED_EDGE ( 'NONE', *, *, #46215, .T. ) ;
#23395=DIRECTION ( 'NONE',  ( -1.655270492344281801E-16, 1.000000000000000000, 0.000000000000000000 ) ) ;
#23427=VERTEX_POINT ( 'NONE', #17779 ) ;
#23592=ORIENTED_EDGE ( 'NONE', *, *, #37834, .T. ) ;
#23636=EDGE_CURVE ( 'NONE', #35697, #33056, #16973, .T. ) ;
#23795=( NAMED_UNIT ( * ) SI_UNIT ( $, .STERADIAN. ) SOLID_ANGLE_UNIT ( ) );
#23838=ORIENTED_EDGE ( 'NONE', *, *, #16154, .T. ) ;
#23842=CARTESIAN_POINT ( 'NONE',  ( -31.75000000000000000, 15.14599999999999369, 0.000000000000000000 ) ) ;
#23889=DIRECTION ( 'NONE',  ( 0.000000000000000000, 0.000000000000000000, 1.000000000000000000 ) ) ;
#23905=CARTESIAN_POINT ( 'NONE',  ( 5.719999999999994422, 15.72000000000000064, 0.000000000000000000 ) ) ;
#23944=CARTESIAN_POINT ( 'NONE',  ( -5.272380000000000067, 0.000000000000000000, 12.55882000000000076 ) ) ;
#24057=CARTESIAN_POINT ( 'NONE',  ( -5.283180000000052168, 0.000000000000000000, 0.000000000000000000 ) ) ;
#24273=ADVANCED_BREP_SHAPE_REPRESENTATION ( '', ( #32179, #14677 ), #31864 ) ;
#24289=VERTEX_POINT ( 'NONE', #42845 ) ;
#24639=CIRCLE ( 'NONE', #42669, 15.71999999999999353 ) ;
#24761=AXIS2_PLACEMENT_3D ( 'NONE', #35329, #49714, #21212 ) ;
#24796=DIRECTION ( 'NONE',  ( 0.000000000000000000, 0.000000000000000000, 1.000000000000000000 ) ) ;
#24820=ORIENTED_EDGE ( 'NONE', *, *, #58726, .T. ) ;
#24955=CARTESIAN_POINT ( 'NONE',  ( 5.272380000000000067, 0.000000000000000000, 12.49999999999999822 ) ) ;
#25072=CARTESIAN_POINT ( 'NONE',  ( 5.331199999999999939, 1.538011871406776419E-15, -12.55882000000000076 ) ) ;
#25107=DIRECTION ( 'NONE',  ( 1.000000000000000000, 1.836909530733573776E-16, 0.000000000000000000 ) ) ;
#25205=CIRCLE ( 'NONE', #59219, 12.55882000000000076 ) ;
#25224=ORIENTED_EDGE ( 'NONE', *, *, #10862, .F. ) ;
#25352=CARTESIAN_POINT ( 'NONE',  ( 5.331200000000000827, 0.000000000000000000, 0.000000000000000000 ) ) ;
#25354=ORIENTED_EDGE ( 'NONE', *, *, #31695, .F. ) ;
#25407=DIRECTION ( 'NONE',  ( -1.626303258728256651E-16, 1.000000000000000000, 0.000000000000000000 ) ) ;
#25416=DIRECTION ( 'NONE',  ( 0.000000000000000000, 0.000000000000000000, 1.000000000000000000 ) ) ;
#25650=AXIS2_PLACEMENT_3D ( 'NONE', #7885, #46131, #22306 ) ;
#25651=CYLINDRICAL_SURFACE ( 'NONE', #34345, 15.14599999999999369 ) ;
#25716=EDGE_CURVE ( 'NONE', #61884, #5803, #56114, .T. ) ;
#25747=VERTEX_POINT ( 'NONE', #22547 ) ;
#25831=AXIS2_PLACEMENT_3D ( 'NONE', #33761, #4584, #18728 ) ;
#25848=AXIS2_PLACEMENT_3D ( 'NONE', #60443, #60148, #55133 ) ;
#25965=DIRECTION ( 'NONE',  ( 0.000000000000000000, 0.000000000000000000, 1.000000000000000000 ) ) ;
#26023=EDGE_LOOP ( 'NONE', ( #34639, #36779 ) ) ;
#26087=CYLINDRICAL_SURFACE ( 'NONE', #47703, 15.43999999999999240 ) ;
#26106=DIRECTION ( 'NONE',  ( 0.000000000000000000, 0.000000000000000000, 1.000000000000000000 ) ) ;
#26156=EDGE_LOOP ( 'NONE', ( #4439, #9, #15157, #33489, #959 ) ) ;
#26381=DIRECTION ( 'NONE',  ( 1.000000000000000000, 1.836909530733573776E-16, 0.000000000000000000 ) ) ;
#26410=CARTESIAN_POINT ( 'NONE',  ( 5.283180000000047727, 0.000000000000000000, 0.000000000000000000 ) ) ;
#26570=CARTESIAN_POINT ( 'NONE',  ( -5.719999999999999751, 4.781475508499492452E-15, 0.000000000000000000 ) ) ;
#26683=AXIS2_PLACEMENT_3D ( 'NONE', #21612, #36352, #60727 ) ;
#26687=VERTEX_POINT ( 'NONE', #57725 ) ;
#26741=APPLICATION_CONTEXT ( 'automotive_design' ) ;
#26762=CARTESIAN_POINT ( 'NONE',  ( 5.719999999999996199, 6.882900011658699842E-15, 0.000000000000000000 ) ) ;
#26779=TOROIDAL_SURFACE ( 'NONE', #12665, 12.55882000000000076, 0.05882000000000109363 ) ;
#26803=ADVANCED_FACE ( 'NONE', ( #22629 ), #28802, .T. ) ;
#26833=AXIS2_PLACEMENT_3D ( 'NONE', #6803, #54736, #12475 ) ;
#27087=EDGE_CURVE ( 'NONE', #18605, #26687, #36835, .T. ) ;
#27117=ORIENTED_EDGE ( 'NONE', *, *, #13975, .T. ) ;
#27121=ADVANCED_FACE ( 'NONE', ( #32819, #8358 ), #31886, .F. ) ;
#27211=DIRECTION ( 'NONE',  ( 0.000000000000000000, -1.000000000000000000, 0.000000000000000000 ) ) ;
#27257=DIRECTION ( 'NONE',  ( -1.000000000000000000, -0.000000000000000000, -0.000000000000000000 ) ) ;
#27362=DIRECTION ( 'NONE',  ( 1.000000000000000000, 1.836909530733573776E-16, 0.000000000000000000 ) ) ;
#27555=DIRECTION ( 'NONE',  ( 0.000000000000000000, -1.000000000000000000, 0.000000000000000000 ) ) ;
#27661=ORIENTED_EDGE ( 'NONE', *, *, #28194, .T. ) ;
#27783=VERTEX_POINT ( 'NONE', #22328 ) ;
#27828=( GEOMETRIC_REPRESENTATION_CONTEXT ( 3 ) GLOBAL_UNCERTAINTY_ASSIGNED_CONTEXT ( ( #47391 ) ) GLOBAL_UNIT_ASSIGNED_CONTEXT ( ( #10315, #9373, #52591 ) ) REPRESENTATION_CONTEXT ( 'NONE', 'WORKASPACE' ) );
#28059=CARTESIAN_POINT ( 'NONE',  ( 5.272379999999998290, 0.000000000000000000, 0.000000000000000000 ) ) ;
#28194=EDGE_CURVE ( 'NONE', #25747, #1919, #9847, .T. ) ;
#28224=LINE ( 'NONE', #23842, #21677 ) ;
#28408=DIRECTION ( 'NONE',  ( 1.000000000000000000, 1.836909530733573776E-16, 0.000000000000000000 ) ) ;
#28550=DIRECTION ( 'NONE',  ( 1.000000000000000000, 1.836909530733573776E-16, 0.000000000000000000 ) ) ;
#28677=ORIENTED_EDGE ( 'NONE', *, *, #2905, .T. ) ;
#28682=DIRECTION ( 'NONE',  ( -0.000000000000000000, 1.000000000000000000, 1.224646799147353207E-16 ) ) ;
#28686=ORIENTED_EDGE ( 'NONE', *, *, #51571, .F. ) ;
#28802=TOROIDAL_SURFACE ( 'NONE', #60799, 15.38217999999999996, 0.05882000000000109363 ) ;
#28803=DIRECTION ( 'NONE',  ( 0.000000000000000000, 0.000000000000000000, 1.000000000000000000 ) ) ;
#28892=CARTESIAN_POINT ( 'NONE',  ( -31.75000000000000000, 16.00000000000000000, 0.000000000000000000 ) ) ;
#28943=( NAMED_UNIT ( * ) PLANE_ANGLE_UNIT ( ) SI_UNIT ( $, .RADIAN. ) );
#29062=AXIS2_PLACEMENT_3D ( 'NONE', #13718, #28408, #32510 ) ;
#29104=( LENGTH_UNIT ( ) NAMED_UNIT ( * ) SI_UNIT ( .MILLI., .METRE. ) );
#29106=CIRCLE ( 'NONE', #2069, 15.14599999999999369 ) ;
#29633=CIRCLE ( 'NONE', #55647, 12.49999999999999822 ) ;
#29840=EDGE_CURVE ( 'NONE', #536, #35413, #25205, .T. ) ;
#29969=CARTESIAN_POINT ( 'NONE',  ( -31.75000000000000000, 0.000000000000000000, 0.000000000000000000 ) ) ;
#30027=CARTESIAN_POINT ( 'NONE',  ( -5.331200000000000827, 0.000000000000000000, 0.000000000000000000 ) ) ;
#30034=DIRECTION ( 'NONE',  ( -1.000000000000000000, -0.000000000000000000, -0.000000000000000000 ) ) ;
#30035=DIRECTION ( 'NONE',  ( -1.000000000000000000, -0.000000000000000000, -0.000000000000000000 ) ) ;
#30071=DIRECTION ( 'NONE',  ( -1.718001593797181987E-16, 1.000000000000000000, 0.000000000000000000 ) ) ;
#30125=ADVANCED_FACE ( 'NONE', ( #6196 ), #11224, .T. ) ;
#30199=ORIENTED_EDGE ( 'NONE', *, *, #54444, .F. ) ;
#30275=CARTESIAN_POINT ( 'NONE',  ( -5.272380000000000067, 0.000000000000000000, 0.000000000000000000 ) ) ;
#30304=ORIENTED_EDGE ( 'NONE', *, *, #21395, .F. ) ;
#30392=ORIENTED_EDGE ( 'NONE', *, *, #60745, .F. ) ;
#30520=EDGE_LOOP ( 'NONE', ( #38895, #45132, #25354, #5161 ) ) ;
#30686=DIRECTION ( 'NONE',  ( 1.000000000000000000, 1.836909530733573776E-16, 0.000000000000000000 ) ) ;
#30746=ORIENTED_EDGE ( 'NONE', *, *, #23636, .T. ) ;
#30751=EDGE_LOOP ( 'NONE', ( #44035, #2219 ) ) ;
#30764=AXIS2_PLACEMENT_3D ( 'NONE', #50354, #41297, #16867 ) ;
#30854=EDGE_CURVE ( 'NONE', #55598, #24289, #44285, .T. ) ;
#30967=DIRECTION ( 'NONE',  ( 0.000000000000000000, 0.000000000000000000, 1.000000000000000000 ) ) ;
#31022=ORIENTED_EDGE ( 'NONE', *, *, #6540, .T. ) ;
#31055=DIRECTION ( 'NONE',  ( 0.000000000000000000, 0.000000000000000000, 1.000000000000000000 ) ) ;
#31169=DIRECTION ( 'NONE',  ( 1.000000000000000000, 1.836909530733573776E-16, 0.000000000000000000 ) ) ;
#31170=DIRECTION ( 'NONE',  ( -1.000000000000000000, -0.000000000000000000, -0.000000000000000000 ) ) ;
#31319=ADVANCED_FACE ( 'NONE', ( #6509 ), #25651, .F. ) ;
#31392=ORIENTED_EDGE ( 'NONE', *, *, #61422, .F. ) ;
#31431=EDGE_LOOP ( 'NONE', ( #37156, #39415, #4304, #19657, #51303 ) ) ;
#31690=EDGE_LOOP ( 'NONE', ( #3776, #59614, #34572, #6598 ) ) ;
#31695=EDGE_CURVE ( 'NONE', #13688, #1749, #61320, .T. ) ;
#31758=EDGE_CURVE ( 'NONE', #48507, #41039, #47347, .T. ) ;
#31841=FACE_OUTER_BOUND ( 'NONE', #50529, .T. ) ;
#31864=( GEOMETRIC_REPRESENTATION_CONTEXT ( 3 ) GLOBAL_UNCERTAINTY_ASSIGNED_CONTEXT ( ( #12976 ) ) GLOBAL_UNIT_ASSIGNED_CONTEXT ( ( #29104, #264, #23795 ) ) REPRESENTATION_CONTEXT ( 'NONE', 'WORKASPACE' ) );
#31886=PLANE ( 'NONE',  #20805 ) ;
#31899=DIRECTION ( 'NONE',  ( -1.626303258728256651E-16, 1.000000000000000000, 0.000000000000000000 ) ) ;
#31973=EDGE_CURVE ( 'NONE', #23427, #41881, #36324, .T. ) ;
#31976=AXIS2_PLACEMENT_3D ( 'NONE', #24057, #57536, #58465 ) ;
#32044=PLANE ( 'NONE',  #39853 ) ;
#32111=LINE ( 'NONE', #45596, #61360 ) ;
#32121=EDGE_CURVE ( 'NONE', #46997, #18605, #32111, .T. ) ;
#32135=EDGE_LOOP ( 'NONE', ( #16046, #7719 ) ) ;
#32179=MANIFOLD_SOLID_BREP ( 'RollersSimplified', #3994 ) ;
#32235=EDGE_LOOP ( 'NONE', ( #3947, #13970 ) ) ;
#32332=DIRECTION ( 'NONE',  ( 1.000000000000000000, 1.836909530733573776E-16, 0.000000000000000000 ) ) ;
#32342=DIRECTION ( 'NONE',  ( 0.000000000000000000, 0.000000000000000000, 1.000000000000000000 ) ) ;
#32386=CIRCLE ( 'NONE', #5342, 15.99999999999999645 ) ;
#32420=ADVANCED_FACE ( 'NONE', ( #46682 ), #7827, .F. ) ;
#32510=DIRECTION ( 'NONE',  ( 0.000000000000000000, 1.000000000000000000, 0.000000000000000000 ) ) ;
#32616=CARTESIAN_POINT ( 'NONE',  ( 6.000000000000000888, -15.14599999999998658, 1.854850041988580043E-15 ) ) ;
#32622=ORIENTED_EDGE ( 'NONE', *, *, #2595, .T. ) ;
#32688=AXIS2_PLACEMENT_3D ( 'NONE', #36832, #2971, #16789 ) ;
#32819=FACE_BOUND ( 'NONE', #3085, .T. ) ;
#32974=CARTESIAN_POINT ( 'NONE',  ( -6.000000000000001776, 4.730042041638951881E-15, 0.000000000000000000 ) ) ;
#33014=FACE_OUTER_BOUND ( 'NONE', #51200, .T. ) ;
#33015=DIRECTION ( 'NONE',  ( 0.000000000000000000, 0.000000000000000000, -1.000000000000000000 ) ) ;
#33056=VERTEX_POINT ( 'NONE', #24955 ) ;
#33080=DIRECTION ( 'NONE',  ( 0.000000000000000000, -1.224646799147364547E-16, 1.000000000000000000 ) ) ;
#33120=DIRECTION ( 'NONE',  ( 1.000000000000000000, 1.836909530733573776E-16, 0.000000000000000000 ) ) ;
#33195=DIRECTION ( 'NONE',  ( 1.000000000000000000, 1.836909530733573776E-16, 0.000000000000000000 ) ) ;
#33317=ORIENTED_EDGE ( 'NONE', *, *, #29840, .F. ) ;
#33345=ORIENTED_EDGE ( 'NONE', *, *, #40204, .T. ) ;
#33361=DIRECTION ( 'NONE',  ( 0.000000000000000000, -1.000000000000000000, 0.000000000000000000 ) ) ;
#33453=FACE_OUTER_BOUND ( 'NONE', #48334, .T. ) ;
#33489=ORIENTED_EDGE ( 'NONE', *, *, #40009, .T. ) ;
#33503=FACE_OUTER_BOUND ( 'NONE', #17073, .T. ) ;
#33509=AXIS2_PLACEMENT_3D ( 'NONE', #37541, #43476, #61911 ) ;
#33614=DIRECTION ( 'NONE',  ( 1.000000000000000000, 1.836909530733573776E-16, 0.000000000000000000 ) ) ;
#33632=AXIS2_PLACEMENT_3D ( 'NONE', #14297, #28682, #38118 ) ;
#33697=ORIENTED_EDGE ( 'NONE', *, *, #12914, .T. ) ;
#33761=CARTESIAN_POINT ( 'NONE',  ( 5.719999999999996199, 6.882900011658699842E-15, 0.000000000000000000 ) ) ;
#33775=CARTESIAN_POINT ( 'NONE',  ( -25.39999999999999858, 1.530808498934191324E-15, -12.49999999999999822 ) ) ;
#33794=CIRCLE ( 'NONE', #30764, 0.05882000000000109363 ) ;
#33826=PRESENTATION_STYLE_ASSIGNMENT (( #14105 ) ) ;
#33890=CARTESIAN_POINT ( 'NONE',  ( -25.39999999999999858, 0.000000000000000000, 0.000000000000000000 ) ) ;
#34003=DIRECTION ( 'NONE',  ( -2.249565377136137858E-32, 1.224646799147353207E-16, 1.000000000000000000 ) ) ;
#34177=CARTESIAN_POINT ( 'NONE',  ( 5.440000000000000391, 6.831466544798160849E-15, 0.000000000000000000 ) ) ;
#34281=DIRECTION ( 'NONE',  ( -1.000000000000000000, -1.836909530733573776E-16, 0.000000000000000000 ) ) ;
#34345=AXIS2_PLACEMENT_3D ( 'NONE', #59152, #16261, #35385 ) ;
#34404=ORIENTED_EDGE ( 'NONE', *, *, #128, .F. ) ;
#34463=APPLICATION_CONTEXT ( 'automotive_design' ) ;
#34473=ORIENTED_EDGE ( 'NONE', *, *, #46215, .F. ) ;
#34509=CIRCLE ( 'NONE', #61475, 15.43999999999999240 ) ;
#34572=ORIENTED_EDGE ( 'NONE', *, *, #56171, .T. ) ;
#34639=ORIENTED_EDGE ( 'NONE', *, *, #15957, .T. ) ;
#34821=FILL_AREA_STYLE ('',( #37441 ) ) ;
#34838=AXIS2_PLACEMENT_3D ( 'NONE', #6894, #34281, #48068 ) ;
#34856=CARTESIAN_POINT ( 'NONE',  ( 5.331200000000000827, 0.000000000000000000, 15.38217999999999996 ) ) ;
#34975=CYLINDRICAL_SURFACE ( 'NONE', #2585, 15.43999999999999240 ) ;
#35047=ORIENTED_EDGE ( 'NONE', *, *, #23064, .F. ) ;
#35074=CIRCLE ( 'NONE', #42062, 0.05882000000000109363 ) ;
#35137=CARTESIAN_POINT ( 'NONE',  ( -5.331200000000000827, 0.000000000000000000, 0.000000000000000000 ) ) ;
#35295=ORIENTED_EDGE ( 'NONE', *, *, #54980, .T. ) ;
#35329=CARTESIAN_POINT ( 'NONE',  ( -5.440000000000000391, 4.832908975360033023E-15, 0.000000000000000000 ) ) ;
#35380=( GEOMETRIC_REPRESENTATION_CONTEXT ( 3 ) GLOBAL_UNCERTAINTY_ASSIGNED_CONTEXT ( ( #43020 ) ) GLOBAL_UNIT_ASSIGNED_CONTEXT ( ( #52425, #28943, #11010 ) ) REPRESENTATION_CONTEXT ( 'NONE', 'WORKASPACE' ) );
#35385=DIRECTION ( 'NONE',  ( 0.000000000000000000, 1.000000000000000000, 0.000000000000000000 ) ) ;
#35413=VERTEX_POINT ( 'NONE', #10909 ) ;
#35490=EDGE_LOOP ( 'NONE', ( #30304, #30746, #22681, #58539 ) ) ;
#35697=VERTEX_POINT ( 'NONE', #15530 ) ;
#35720=ORIENTED_EDGE ( 'NONE', *, *, #57156, .F. ) ;
#35847=VERTEX_POINT ( 'NONE', #8489 ) ;
#35872=CARTESIAN_POINT ( 'NONE',  ( -5.440000000000000391, 4.832908975360033023E-15, 0.000000000000000000 ) ) ;
#35906=ADVANCED_FACE ( 'NONE', ( #51097 ), #8189, .T. ) ;
#35997=ADVANCED_FACE ( 'NONE', ( #42654 ), #26779, .T. ) ;
#36148=CIRCLE ( 'NONE', #38171, 16.00000000000000000 ) ;
#36152=ORIENTED_EDGE ( 'NONE', *, *, #4289, .T. ) ;
#36183=DIRECTION ( 'NONE',  ( 1.000000000000000000, 1.836909530733573776E-16, 0.000000000000000000 ) ) ;
#36233=DIRECTION ( 'NONE',  ( 1.000000000000000000, 1.836909530733573776E-16, 0.000000000000000000 ) ) ;
#36250=EDGE_LOOP ( 'NONE', ( #3167, #4712 ) ) ;
#36277=VECTOR ( 'NONE', #36972, 1000.000000000000000 ) ;
#36285=DIRECTION ( 'NONE',  ( 1.000000000000000000, 0.000000000000000000, 0.000000000000000000 ) ) ;
#36300=DIRECTION ( 'NONE',  ( 1.000000000000000000, 1.836909530733573776E-16, 0.000000000000000000 ) ) ;
#36324=CIRCLE ( 'NONE', #6254, 15.71999999999999709 ) ;
#36352=DIRECTION ( 'NONE',  ( 1.000000000000000000, 0.000000000000000000, 0.000000000000000000 ) ) ;
#36400=ORIENTED_EDGE ( 'NONE', *, *, #12914, .F. ) ;
#36507=AXIS2_PLACEMENT_3D ( 'NONE', #61581, #43449, #23395 ) ;
#36683=CIRCLE ( 'NONE', #33632, 0.05882000000000109363 ) ;
#36692=EDGE_CURVE ( 'NONE', #41039, #11235, #40809, .T. ) ;
#36760=CARTESIAN_POINT ( 'NONE',  ( 5.999999999999998224, 6.934333478519240412E-15, 0.000000000000000000 ) ) ;
#36779=ORIENTED_EDGE ( 'NONE', *, *, #11776, .T. ) ;
#36832=CARTESIAN_POINT ( 'NONE',  ( 5.283180000000047727, 0.000000000000000000, 0.000000000000000000 ) ) ;
#36835=CIRCLE ( 'NONE', #26833, 0.2800000000000024691 ) ;
#36972=DIRECTION ( 'NONE',  ( 1.000000000000000000, 1.836909530733573776E-16, 0.000000000000000000 ) ) ;
#36999=CARTESIAN_POINT ( 'NONE',  ( -5.272380000000000067, 0.000000000000000000, 12.49999999999999822 ) ) ;
#37027=ORIENTED_EDGE ( 'NONE', *, *, #32121, .F. ) ;
#37090=EDGE_LOOP ( 'NONE', ( #7726, #9038 ) ) ;
#37149=SHAPE_DEFINITION_REPRESENTATION ( #17805, #10831 ) ;
#37156=ORIENTED_EDGE ( 'NONE', *, *, #36692, .F. ) ;
#37182=CARTESIAN_POINT ( 'NONE',  ( -5.272380000000000067, 0.000000000000000000, 0.000000000000000000 ) ) ;
#37233=ADVANCED_FACE ( 'NONE', ( #6955 ), #26087, .F. ) ;
#37441=FILL_AREA_STYLE_COLOUR ( '', #7338 ) ;
#37541=CARTESIAN_POINT ( 'NONE',  ( -31.75000000000000000, 0.000000000000000000, 0.000000000000000000 ) ) ;
#37610=DIRECTION ( 'NONE',  ( 1.000000000000000000, 1.836909530733573776E-16, 0.000000000000000000 ) ) ;
#37764=CIRCLE ( 'NONE', #24761, 15.43999999999999417 ) ;
#37789=EDGE_CURVE ( 'NONE', #39188, #27783, #59669, .T. ) ;
#37834=EDGE_CURVE ( 'NONE', #35413, #13688, #2654, .T. ) ;
#38001=CIRCLE ( 'NONE', #59958, 0.05882000000000109363 ) ;
#38021=DIRECTION ( 'NONE',  ( 1.000000000000000000, 1.836909530733573776E-16, 0.000000000000000000 ) ) ;
#38026=DIRECTION ( 'NONE',  ( 1.836909530733573776E-16, -1.000000000000000000, 0.000000000000000000 ) ) ;
#38118=DIRECTION ( 'NONE',  ( 0.000000000000000000, -1.224646799147332007E-16, 1.000000000000000000 ) ) ;
#38171=AXIS2_PLACEMENT_3D ( 'NONE', #49215, #11319, #25407 ) ;
#38226=FILL_AREA_STYLE ('',( #15333 ) ) ;
#38331=DIRECTION ( 'NONE',  ( -0.000000000000000000, 0.000000000000000000, 1.000000000000000000 ) ) ;
#38390=ORIENTED_EDGE ( 'NONE', *, *, #27087, .F. ) ;
#38424=DIRECTION ( 'NONE',  ( 0.000000000000000000, 1.000000000000000000, 0.000000000000000000 ) ) ;
#38497=CIRCLE ( 'NONE', #46492, 0.05882000000000109363 ) ;
#38505=ORIENTED_EDGE ( 'NONE', *, *, #52897, .F. ) ;
#38541=ORIENTED_EDGE ( 'NONE', *, *, #16602, .T. ) ;
#38647=AXIS2_PLACEMENT_3D ( 'NONE', #20448, #54545, #43983 ) ;
#38788=AXIS2_PLACEMENT_3D ( 'NONE', #20452, #26381, #59263 ) ;
#38806=DIRECTION ( 'NONE',  ( 1.000000000000000000, 1.836909530733573776E-16, 0.000000000000000000 ) ) ;
#38870=ORIENTED_EDGE ( 'NONE', *, *, #61422, .T. ) ;
#38895=ORIENTED_EDGE ( 'NONE', *, *, #40193, .T. ) ;
#38939=CARTESIAN_POINT ( 'NONE',  ( 5.272379999999998290, 0.000000000000000000, 0.000000000000000000 ) ) ;
#38942=PRODUCT_DEFINITION_FORMATION_WITH_SPECIFIED_SOURCE ( 'ANY', '', #16255, .NOT_KNOWN. ) ;
#38944=ORIENTED_EDGE ( 'NONE', *, *, #21395, .T. ) ;
#38956=VERTEX_POINT ( 'NONE', #2078 ) ;
#39031=EDGE_CURVE ( 'NONE', #8791, #1476, #37764, .T. ) ;
#39188=VERTEX_POINT ( 'NONE', #792 ) ;
#39216=FACE_OUTER_BOUND ( 'NONE', #20146, .T. ) ;
#39395=FACE_OUTER_BOUND ( 'NONE', #59178, .T. ) ;
#39415=ORIENTED_EDGE ( 'NONE', *, *, #128, .T. ) ;
#39492=DIRECTION ( 'NONE',  ( 1.000000000000000000, 1.836909530733573776E-16, 0.000000000000000000 ) ) ;
#39514=AXIS2_PLACEMENT_3D ( 'NONE', #33890, #48283, #52966 ) ;
#39551=TOROIDAL_SURFACE ( 'NONE', #8477, 15.38217999999999996, 0.05882000000000109363 ) ;
#39593=ORIENTED_EDGE ( 'NONE', *, *, #54980, .F. ) ;
#39619=ORIENTED_EDGE ( 'NONE', *, *, #49652, .F. ) ;
#39693=EDGE_CURVE ( 'NONE', #8791, #11235, #8733, .T. ) ;
#39698=AXIS2_PLACEMENT_3D ( 'NONE', #40397, #59459, #25965 ) ;
#39844=ORIENTED_EDGE ( 'NONE', *, *, #49652, .T. ) ;
#39853=AXIS2_PLACEMENT_3D ( 'NONE', #54965, #46767, #41766 ) ;
#39960=ORIENTED_EDGE ( 'NONE', *, *, #51332, .T. ) ;
#39977=ORIENTED_EDGE ( 'NONE', *, *, #18541, .F. ) ;
#40009=EDGE_CURVE ( 'NONE', #2478, #19981, #7622, .T. ) ;
#40193=EDGE_CURVE ( 'NONE', #35413, #536, #51626, .T. ) ;
#40204=EDGE_CURVE ( 'NONE', #1749, #13688, #29633, .T. ) ;
#40246=DIRECTION ( 'NONE',  ( -1.000000000000000000, -0.000000000000000000, -0.000000000000000000 ) ) ;
#40255=ORIENTED_EDGE ( 'NONE', *, *, #40204, .F. ) ;
#40270=TOROIDAL_SURFACE ( 'NONE', #14233, 15.38217999999999996, 0.05882000000000066342 ) ;
#40395=STYLED_ITEM ( 'NONE', ( #19559 ), #32179 ) ;
#40397=CARTESIAN_POINT ( 'NONE',  ( -5.272380000000000067, 0.000000000000000000, 0.000000000000000000 ) ) ;
#40440=VERTEX_POINT ( 'NONE', #14238 ) ;
#40577=VECTOR ( 'NONE', #33614, 1000.000000000000000 ) ;
#40809=CIRCLE ( 'NONE', #13791, 15.43999999999999240 ) ;
#40919=DIRECTION ( 'NONE',  ( 0.000000000000000000, 0.000000000000000000, 1.000000000000000000 ) ) ;
#40957=ORIENTED_EDGE ( 'NONE', *, *, #4761, .T. ) ;
#40968=VERTEX_POINT ( 'NONE', #5532 ) ;
#41039=VERTEX_POINT ( 'NONE', #54690 ) ;
#41105=ORIENTED_EDGE ( 'NONE', *, *, #60165, .F. ) ;
#41134=CARTESIAN_POINT ( 'NONE',  ( -5.719999999999997087, -15.99999999999999645, 1.959434878635764737E-15 ) ) ;
#41252=DIRECTION ( 'NONE',  ( 0.000000000000000000, 0.000000000000000000, 1.000000000000000000 ) ) ;
#41297=DIRECTION ( 'NONE',  ( -0.000000000000000000, 1.000000000000000000, 1.224646799147353207E-16 ) ) ;
#41649=CARTESIAN_POINT ( 'NONE',  ( -5.999999999999999112, -15.71999999999999353, 1.942289823447701879E-15 ) ) ;
#41766=DIRECTION ( 'NONE',  ( -1.836909530733573776E-16, 1.000000000000000000, 0.000000000000000000 ) ) ;
#41881=VERTEX_POINT ( 'NONE', #41649 ) ;
#41900=DIRECTION ( 'NONE',  ( -1.685288351013738396E-16, 1.000000000000000000, 0.000000000000000000 ) ) ;
#41973=ORIENTED_EDGE ( 'NONE', *, *, #45155, .F. ) ;
#41976=DIRECTION ( 'NONE',  ( 1.000000000000000000, 1.836909530733573776E-16, 0.000000000000000000 ) ) ;
#42062=AXIS2_PLACEMENT_3D ( 'NONE', #22283, #60169, #54527 ) ;
#42318=AXIS2_PLACEMENT_3D ( 'NONE', #6317, #15769, #44597 ) ;
#42364=ORIENTED_EDGE ( 'NONE', *, *, #32121, .T. ) ;
#42509=ORIENTED_EDGE ( 'NONE', *, *, #20579, .F. ) ;
#42529=DIRECTION ( 'NONE',  ( 0.000000000000000000, 0.000000000000000000, -1.000000000000000000 ) ) ;
#42596=DIRECTION ( 'NONE',  ( 0.000000000000000000, 0.000000000000000000, -1.000000000000000000 ) ) ;
#42607=SHAPE_REPRESENTATION_RELATIONSHIP ( 'NONE' , 'NONE' ,  #10831, #24273 ) ;
#42654=FACE_OUTER_BOUND ( 'NONE', #35490, .T. ) ;
#42669=AXIS2_PLACEMENT_3D ( 'NONE', #4610, #38806, #5239 ) ;
#42672=AXIS2_PLACEMENT_3D ( 'NONE', #59037, #50569, #16450 ) ;
#42678=DIRECTION ( 'NONE',  ( -1.655270492344281801E-16, 1.000000000000000000, 0.000000000000000000 ) ) ;
#42845=CARTESIAN_POINT ( 'NONE',  ( -5.439999999999997726, -15.14599999999999014, 1.854850041988580438E-15 ) ) ;
#42898=CARTESIAN_POINT ( 'NONE',  ( -31.75000000000000000, 15.43999999999999240, 0.000000000000000000 ) ) ;
#42948=VERTEX_POINT ( 'NONE', #45067 ) ;
#42982=AXIS2_PLACEMENT_3D ( 'NONE', #679, #38021, #4743 ) ;
#43018=FACE_OUTER_BOUND ( 'NONE', #12044, .T. ) ;
#43020=UNCERTAINTY_MEASURE_WITH_UNIT (LENGTH_MEASURE( 1.000000000000000082E-05 ), #52425, 'distance_accuracy_value', 'NONE');
#43023=LINE ( 'NONE', #28892, #40577 ) ;
#43036=DIRECTION ( 'NONE',  ( -1.000000000000000000, 0.000000000000000000, 0.000000000000000000 ) ) ;
#43130=ORIENTED_EDGE ( 'NONE', *, *, #29840, .T. ) ;
#43332=FACE_OUTER_BOUND ( 'NONE', #32135, .T. ) ;
#43449=DIRECTION ( 'NONE',  ( 1.000000000000000000, 1.836909530733573776E-16, 0.000000000000000000 ) ) ;
#43476=DIRECTION ( 'NONE',  ( 1.000000000000000000, 1.836909530733573776E-16, 0.000000000000000000 ) ) ;
#43569=AXIS2_PLACEMENT_3D ( 'NONE', #13274, #51769, #38026 ) ;
#43723=ORIENTED_EDGE ( 'NONE', *, *, #20055, .F. ) ;
#43752=CARTESIAN_POINT ( 'NONE',  ( -31.75000000000000000, 0.000000000000000000, 0.000000000000000000 ) ) ;
#43809=ORIENTED_EDGE ( 'NONE', *, *, #20579, .T. ) ;
#43983=DIRECTION ( 'NONE',  ( -1.836909530733573776E-16, 1.000000000000000000, 0.000000000000000000 ) ) ;
#44035=ORIENTED_EDGE ( 'NONE', *, *, #4761, .F. ) ;
#44077=CARTESIAN_POINT ( 'NONE',  ( -5.283180000000052168, 0.000000000000000000, 0.000000000000000000 ) ) ;
#44111=DIRECTION ( 'NONE',  ( 1.000000000000000000, 1.836909530733573776E-16, 0.000000000000000000 ) ) ;
#44285=CIRCLE ( 'NONE', #48288, 15.14599999999999369 ) ;
#44293=FACE_OUTER_BOUND ( 'NONE', #47031, .T. ) ;
#44389=CARTESIAN_POINT ( 'NONE',  ( -31.75000000000000000, 0.000000000000000000, 0.000000000000000000 ) ) ;
#44403=CARTESIAN_POINT ( 'NONE',  ( -5.272380000000000067, 0.000000000000000000, 15.38217999999999996 ) ) ;
#44475=DIRECTION ( 'NONE',  ( -1.000000000000000000, -0.000000000000000000, -0.000000000000000000 ) ) ;
#44547=AXIS2_PLACEMENT_3D ( 'NONE', #12419, #51525, #33080 ) ;
#44597=DIRECTION ( 'NONE',  ( 0.000000000000000000, 1.000000000000000000, 0.000000000000000000 ) ) ;
#44650=AXIS2_PLACEMENT_3D ( 'NONE', #26570, #36300, #31899 ) ;
#44791=FACE_OUTER_BOUND ( 'NONE', #51935, .T. ) ;
#44814=ORIENTED_EDGE ( 'NONE', *, *, #40193, .F. ) ;
#44897=COLOUR_RGB ( '', 0.31764706, 0.68627451, 0.89019608) ;
#44969=ORIENTED_EDGE ( 'NONE', *, *, #54444, .T. ) ;
#45067=CARTESIAN_POINT ( 'NONE',  ( 5.439999999999997726, 15.14599999999999902, 0.000000000000000000 ) ) ;
#45132=ORIENTED_EDGE ( 'NONE', *, *, #60745, .T. ) ;
#45155=EDGE_CURVE ( 'NONE', #33056, #5641, #12001, .T. ) ;
#45221=EDGE_CURVE ( 'NONE', #38956, #48507, #48997, .T. ) ;
#45335=DIRECTION ( 'NONE',  ( -1.000000000000000000, -0.000000000000000000, -0.000000000000000000 ) ) ;
#45525=CARTESIAN_POINT ( 'NONE',  ( -5.272380000000000067, 0.000000000000000000, 0.000000000000000000 ) ) ;
#45596=CARTESIAN_POINT ( 'NONE',  ( -31.75000000000000000, -16.00000000000000000, 1.959434878635765131E-15 ) ) ;
#45722=EDGE_LOOP ( 'NONE', ( #28677, #42364, #13176, #51613 ) ) ;
#45733=CIRCLE ( 'NONE', #58696, 15.14599999999999369 ) ;
#45807=TOROIDAL_SURFACE ( 'NONE', #9778, 15.71999999999999709, 0.2800000000000011924 ) ;
#45970=DIRECTION ( 'NONE',  ( 0.000000000000000000, 0.000000000000000000, 1.000000000000000000 ) ) ;
#46045=AXIS2_PLACEMENT_3D ( 'NONE', #58730, #31170, #40919 ) ;
#46131=DIRECTION ( 'NONE',  ( 1.000000000000000000, 1.836909530733573776E-16, 0.000000000000000000 ) ) ;
#46159=DIRECTION ( 'NONE',  ( -1.718001593797181987E-16, 1.000000000000000000, 0.000000000000000000 ) ) ;
#46215=EDGE_CURVE ( 'NONE', #33056, #35697, #56003, .T. ) ;
#46250=CIRCLE ( 'NONE', #61196, 15.38217999999999996 ) ;
#46254=CARTESIAN_POINT ( 'NONE',  ( -5.283180000000052168, 0.000000000000000000, 0.000000000000000000 ) ) ;
#46338=DIRECTION ( 'NONE',  ( 0.000000000000000000, 0.000000000000000000, -1.000000000000000000 ) ) ;
#46391=CIRCLE ( 'NONE', #59367, 15.43999999999999417 ) ;
#46492=AXIS2_PLACEMENT_3D ( 'NONE', #44403, #16179, #1430 ) ;
#46609=CIRCLE ( 'NONE', #61592, 0.2800000000000007483 ) ;
#46682=FACE_OUTER_BOUND ( 'NONE', #22973, .T. ) ;
#46760=DIRECTION ( 'NONE',  ( 0.000000000000000000, 1.000000000000000000, 0.000000000000000000 ) ) ;
#46767=DIRECTION ( 'NONE',  ( 1.000000000000000000, 1.836909530733573776E-16, 0.000000000000000000 ) ) ;
#46816=AXIS2_PLACEMENT_3D ( 'NONE', #20644, #30035, #30967 ) ;
#46850=EDGE_CURVE ( 'NONE', #24289, #55598, #47758, .T. ) ;
#46883=CARTESIAN_POINT ( 'NONE',  ( -5.331200000000000827, 1.538011871406776419E-15, -12.55882000000000076 ) ) ;
#46913=CIRCLE ( 'NONE', #13904, 15.38218000000000174 ) ;
#46959=CIRCLE ( 'NONE', #59939, 15.43999999999999240 ) ;
#46997=VERTEX_POINT ( 'NONE', #41134 ) ;
#47031=EDGE_LOOP ( 'NONE', ( #43723, #7298, #32622, #31392 ) ) ;
#47121=CARTESIAN_POINT ( 'NONE',  ( -5.720000000000002416, 16.00000000000000355, 0.000000000000000000 ) ) ;
#47297=CARTESIAN_POINT ( 'NONE',  ( 5.719999999999997087, 6.938893903907228378E-15, 0.000000000000000000 ) ) ;
#47341=DIRECTION ( 'NONE',  ( 1.000000000000000000, 1.836909530733573776E-16, 0.000000000000000000 ) ) ;
#47347=CIRCLE ( 'NONE', #11310, 15.43999999999999240 ) ;
#47391=UNCERTAINTY_MEASURE_WITH_UNIT (LENGTH_MEASURE( 1.000000000000000082E-05 ), #10315, 'distance_accuracy_value', 'NONE');
#47407=CIRCLE ( 'NONE', #2354, 15.14599999999999369 ) ;
#47443=CYLINDRICAL_SURFACE ( 'NONE', #13806, 16.00000000000000000 ) ;
#47503=ADVANCED_FACE ( 'NONE', ( #33503 ), #45807, .T. ) ;
#47517=AXIS2_PLACEMENT_3D ( 'NONE', #29969, #44111, #6742 ) ;
#47534=DIRECTION ( 'NONE',  ( -1.718001593797181987E-16, 1.000000000000000000, 0.000000000000000000 ) ) ;
#47665=TOROIDAL_SURFACE ( 'NONE', #18654, 12.55882000000000076, 0.05882000000000066342 ) ;
#47702=FACE_BOUND ( 'NONE', #32235, .T. ) ;
#47703=AXIS2_PLACEMENT_3D ( 'NONE', #2260, #9137, #46760 ) ;
#47758=CIRCLE ( 'NONE', #38788, 15.14599999999999369 ) ;
#48023=PLANE ( 'NONE',  #14107 ) ;
#48059=SURFACE_SIDE_STYLE ('',( #9839 ) ) ;
#48068=DIRECTION ( 'NONE',  ( 1.836909530733573776E-16, -1.000000000000000000, 0.000000000000000000 ) ) ;
#48172=DIRECTION ( 'NONE',  ( -1.000000000000000000, -0.000000000000000000, -0.000000000000000000 ) ) ;
#48272=DIRECTION ( 'NONE',  ( 0.000000000000000000, 0.000000000000000000, 1.000000000000000000 ) ) ;
#48281=CARTESIAN_POINT ( 'NONE',  ( -5.440000000000003055, 15.14599999999999902, 0.000000000000000000 ) ) ;
#48283=DIRECTION ( 'NONE',  ( -1.000000000000000000, -0.000000000000000000, -0.000000000000000000 ) ) ;
#48288=AXIS2_PLACEMENT_3D ( 'NONE', #58595, #25107, #11324 ) ;
#48300=ADVANCED_FACE ( 'NONE', ( #15401 ), #48824, .T. ) ;
#48334=EDGE_LOOP ( 'NONE', ( #39593, #35720, #31022, #1863 ) ) ;
#48364=ORIENTED_EDGE ( 'NONE', *, *, #36692, .T. ) ;
#48380=ORIENTED_EDGE ( 'NONE', *, *, #45221, .T. ) ;
#48507=VERTEX_POINT ( 'NONE', #3732 ) ;
#48555=CIRCLE ( 'NONE', #21560, 0.2800000000000007483 ) ;
#48712=ORIENTED_EDGE ( 'NONE', *, *, #23090, .T. ) ;
#48713=DIRECTION ( 'NONE',  ( -1.000000000000000000, -0.000000000000000000, -0.000000000000000000 ) ) ;
#48734=DIRECTION ( 'NONE',  ( 1.000000000000000000, 0.000000000000000000, 0.000000000000000000 ) ) ;
#48824=TOROIDAL_SURFACE ( 'NONE', #4736, 15.71999999999999353, 0.2800000000000011924 ) ;
#48873=EDGE_CURVE ( 'NONE', #40968, #26687, #22844, .T. ) ;
#48912=CARTESIAN_POINT ( 'NONE',  ( -6.000000000000001776, 4.730042041638951881E-15, 0.000000000000000000 ) ) ;
#48997=CIRCLE ( 'NONE', #31976, 15.43999999999999240 ) ;
#49086=LINE ( 'NONE', #33775, #4172 ) ;
#49127=ADVANCED_FACE ( 'NONE', ( #10157, #57427 ), #4810, .T. ) ;
#49215=CARTESIAN_POINT ( 'NONE',  ( -5.719999999999999751, 4.781475508499492452E-15, 0.000000000000000000 ) ) ;
#49288=ADVANCED_FACE ( 'NONE', ( #4044 ), #49847, .T. ) ;
#49339=CARTESIAN_POINT ( 'NONE',  ( -5.272380000000000067, 0.000000000000000000, 0.000000000000000000 ) ) ;
#49354=DIRECTION ( 'NONE',  ( 0.000000000000000000, 1.000000000000000000, 0.000000000000000000 ) ) ;
#49408=CARTESIAN_POINT ( 'NONE',  ( 5.272380000000000067, 0.000000000000000000, 0.000000000000000000 ) ) ;
#49420=VERTEX_POINT ( 'NONE', #15953 ) ;
#49595=CARTESIAN_POINT ( 'NONE',  ( 5.283180000000047727, 0.000000000000000000, 0.000000000000000000 ) ) ;
#49652=EDGE_CURVE ( 'NONE', #18605, #3794, #5820, .T. ) ;
#49677=TOROIDAL_SURFACE ( 'NONE', #39698, 12.55882000000000076, 0.05882000000000066342 ) ;
#49686=CYLINDRICAL_SURFACE ( 'NONE', #47517, 15.43999999999999240 ) ;
#49714=DIRECTION ( 'NONE',  ( 1.000000000000000000, 1.836909530733573776E-16, 0.000000000000000000 ) ) ;
#49808=ORIENTED_EDGE ( 'NONE', *, *, #18541, .T. ) ;
#49847=TOROIDAL_SURFACE ( 'NONE', #7806, 15.71999999999999353, 0.2800000000000011924 ) ;
#49953=FACE_OUTER_BOUND ( 'NONE', #31431, .T. ) ;
#50101=DIRECTION ( 'NONE',  ( -1.718001593797181987E-16, 1.000000000000000000, 0.000000000000000000 ) ) ;
#50354=CARTESIAN_POINT ( 'NONE',  ( 5.272379999999998290, 1.883773750090843600E-15, -15.38217999999999996 ) ) ;
#50436=EDGE_LOOP ( 'NONE', ( #18419, #48712, #56036, #48364, #61180 ) ) ;
#50529=EDGE_LOOP ( 'NONE', ( #33697, #49808, #4325, #14456, #35047 ) ) ;
#50569=DIRECTION ( 'NONE',  ( -1.000000000000000000, -0.000000000000000000, -0.000000000000000000 ) ) ;
#50572=EDGE_LOOP ( 'NONE', ( #37027, #27117, #24820, #39619 ) ) ;
#50854=LINE ( 'NONE', #2615, #58969 ) ;
#50860=ORIENTED_EDGE ( 'NONE', *, *, #6540, .F. ) ;
#50921=DIRECTION ( 'NONE',  ( 0.000000000000000000, 0.000000000000000000, -1.000000000000000000 ) ) ;
#51037=LINE ( 'NONE', #3415, #60941 ) ;
#51043=CARTESIAN_POINT ( 'NONE',  ( -25.39999999999999858, 0.000000000000000000, 0.000000000000000000 ) ) ;
#51097=FACE_OUTER_BOUND ( 'NONE', #50572, .T. ) ;
#51119=CARTESIAN_POINT ( 'NONE',  ( -5.272380000000000067, 1.534410185170483674E-15, -12.49999999999999822 ) ) ;
#51183=CARTESIAN_POINT ( 'NONE',  ( 5.440000000000003055, -15.14599999999998658, 1.854850041988580043E-15 ) ) ;
#51200=EDGE_LOOP ( 'NONE', ( #36400, #19943 ) ) ;
#51303=ORIENTED_EDGE ( 'NONE', *, *, #61543, .F. ) ;
#51327=EDGE_CURVE ( 'NONE', #1476, #8791, #46391, .T. ) ;
#51331=FACE_OUTER_BOUND ( 'NONE', #50436, .T. ) ;
#51332=EDGE_CURVE ( 'NONE', #3794, #18605, #32386, .T. ) ;
#51460=CARTESIAN_POINT ( 'NONE',  ( 5.331199999999999051, 15.38217999999999996, 0.000000000000000000 ) ) ;
#51525=DIRECTION ( 'NONE',  ( -0.000000000000000000, 1.000000000000000000, 1.224646799147353207E-16 ) ) ;
#51569=FACE_BOUND ( 'NONE', #37090, .T. ) ;
#51571=EDGE_CURVE ( 'NONE', #42948, #61884, #47407, .T. ) ;
#51613=ORIENTED_EDGE ( 'NONE', *, *, #58726, .F. ) ;
#51626=CIRCLE ( 'NONE', #42672, 12.55882000000000076 ) ;
#51653=CARTESIAN_POINT ( 'NONE',  ( -5.720000000000000639, 3.469446951953614189E-15, 0.000000000000000000 ) ) ;
#51660=PRODUCT_DEFINITION ( 'UNKNOWN', '', #38942, #16042 ) ;
#51672=DIRECTION ( 'NONE',  ( -1.836909530733573776E-16, 1.000000000000000000, 0.000000000000000000 ) ) ;
#51720=CARTESIAN_POINT ( 'NONE',  ( 5.272379999999998290, 0.000000000000000000, 0.000000000000000000 ) ) ;
#51769=DIRECTION ( 'NONE',  ( -1.000000000000000000, -1.836909530733573776E-16, 0.000000000000000000 ) ) ;
#51850=DIRECTION ( 'NONE',  ( -1.000000000000000000, -0.000000000000000000, -0.000000000000000000 ) ) ;
#51935=EDGE_LOOP ( 'NONE', ( #30392, #43130, #23592, #40255 ) ) ;
#51965=DIRECTION ( 'NONE',  ( 1.000000000000000000, 1.836909530733573776E-16, 0.000000000000000000 ) ) ;
#51966=CARTESIAN_POINT ( 'NONE',  ( 5.272379999999998290, 0.000000000000000000, 15.38217999999999996 ) ) ;
#52152=CARTESIAN_POINT ( 'NONE',  ( -5.719999999999997975, -15.71999999999999353, 1.925144768259639022E-15 ) ) ;
#52157=DIRECTION ( 'NONE',  ( 1.000000000000000000, 0.000000000000000000, 0.000000000000000000 ) ) ;
#52218=CYLINDRICAL_SURFACE ( 'NONE', #33509, 15.14599999999999369 ) ;
#52279=SURFACE_SIDE_STYLE ('',( #18798 ) ) ;
#52425=( LENGTH_UNIT ( ) NAMED_UNIT ( * ) SI_UNIT ( .MILLI., .METRE. ) );
#52591=( NAMED_UNIT ( * ) SI_UNIT ( $, .STERADIAN. ) SOLID_ANGLE_UNIT ( ) );
#52657=ADVANCED_FACE ( 'NONE', ( #39216 ), #57963, .F. ) ;
#52722=EDGE_LOOP ( 'NONE', ( #27661, #55005 ) ) ;
#52897=EDGE_CURVE ( 'NONE', #41881, #23427, #18475, .T. ) ;
#52966=DIRECTION ( 'NONE',  ( 0.000000000000000000, 0.000000000000000000, 1.000000000000000000 ) ) ;
#53503=EDGE_CURVE ( 'NONE', #49420, #4994, #57429, .T. ) ;
#53582=DIRECTION ( 'NONE',  ( -1.000000000000000000, -0.000000000000000000, -0.000000000000000000 ) ) ;
#53704=AXIS2_PLACEMENT_3D ( 'NONE', #23944, #33361, #56516 ) ;
#54037=DIRECTION ( 'NONE',  ( 1.000000000000000000, 1.836909530733573776E-16, 0.000000000000000000 ) ) ;
#54040=VECTOR ( 'NONE', #32332, 1000.000000000000000 ) ;
#54130=ADVANCED_FACE ( 'NONE', ( #49953 ), #39551, .T. ) ;
#54138=CARTESIAN_POINT ( 'NONE',  ( 5.283180000000047727, 1.890854657883512518E-15, -15.43999999999999240 ) ) ;
#54189=DIRECTION ( 'NONE',  ( -1.836909530733573776E-16, 1.000000000000000000, 0.000000000000000000 ) ) ;
#54250=CYLINDRICAL_SURFACE ( 'NONE', #42318, 15.14599999999999369 ) ;
#54363=ORIENTED_EDGE ( 'NONE', *, *, #57156, .T. ) ;
#54444=EDGE_CURVE ( 'NONE', #33056, #13688, #55483, .T. ) ;
#54527=DIRECTION ( 'NONE',  ( 0.000000000000000000, -1.224646799147332007E-16, 1.000000000000000000 ) ) ;
#54545=DIRECTION ( 'NONE',  ( 1.000000000000000000, 1.836909530733573776E-16, 0.000000000000000000 ) ) ;
#54569=DIRECTION ( 'NONE',  ( -1.000000000000000000, 0.000000000000000000, 0.000000000000000000 ) ) ;
#54667=CARTESIAN_POINT ( 'NONE',  ( -5.283180000000052168, 15.43999999999999240, 0.000000000000000000 ) ) ;
#54690=CARTESIAN_POINT ( 'NONE',  ( -5.283180000000052168, 1.890854657883512518E-15, -15.43999999999999240 ) ) ;
#54736=DIRECTION ( 'NONE',  ( -2.249565377136137858E-32, 1.224646799147353207E-16, 1.000000000000000000 ) ) ;
#54941=DIRECTION ( 'NONE',  ( -1.685288351013738149E-16, 1.000000000000000000, 0.000000000000000000 ) ) ;
#54965=CARTESIAN_POINT ( 'NONE',  ( 5.999999999999997335, 15.72000000000000064, 0.000000000000000000 ) ) ;
#54980=EDGE_CURVE ( 'NONE', #49420, #24289, #10518, .T. ) ;
#54995=ORIENTED_EDGE ( 'NONE', *, *, #20252, .T. ) ;
#55005=ORIENTED_EDGE ( 'NONE', *, *, #10862, .T. ) ;
#55032=EDGE_LOOP ( 'NONE', ( #21603, #28686, #38870, #40957 ) ) ;
#55133=DIRECTION ( 'NONE',  ( 0.000000000000000000, 0.000000000000000000, 1.000000000000000000 ) ) ;
#55483=LINE ( 'NONE', #22610, #5474 ) ;
#55523=DIRECTION ( 'NONE',  ( 0.000000000000000000, 0.000000000000000000, 1.000000000000000000 ) ) ;
#55598=VERTEX_POINT ( 'NONE', #48281 ) ;
#55647=AXIS2_PLACEMENT_3D ( 'NONE', #49339, #59344, #20846 ) ;
#55660=ORIENTED_EDGE ( 'NONE', *, *, #56171, .F. ) ;
#55797=DIRECTION ( 'NONE',  ( -1.000000000000000000, -0.000000000000000000, -0.000000000000000000 ) ) ;
#55922=ORIENTED_EDGE ( 'NONE', *, *, #37789, .T. ) ;
#56003=CIRCLE ( 'NONE', #4974, 12.49999999999999822 ) ;
#56036=ORIENTED_EDGE ( 'NONE', *, *, #31758, .T. ) ;
#56114=LINE ( 'NONE', #57333, #54040 ) ;
#56171=EDGE_CURVE ( 'NONE', #23427, #61046, #48555, .T. ) ;
#56360=AXIS2_PLACEMENT_3D ( 'NONE', #51043, #27257, #18172 ) ;
#56396=ORIENTED_EDGE ( 'NONE', *, *, #39031, .T. ) ;
#56516=DIRECTION ( 'NONE',  ( 0.000000000000000000, 0.000000000000000000, -1.000000000000000000 ) ) ;
#56637=AXIS2_PLACEMENT_3D ( 'NONE', #8340, #12774, #41900 ) ;
#56990=AXIS2_PLACEMENT_3D ( 'NONE', #60701, #27211, #46338 ) ;
#57156=EDGE_CURVE ( 'NONE', #4994, #49420, #2580, .T. ) ;
#57247=DIRECTION ( 'NONE',  ( 1.000000000000000000, 1.836909530733573776E-16, 0.000000000000000000 ) ) ;
#57333=CARTESIAN_POINT ( 'NONE',  ( -31.75000000000000000, -15.14599999999999369, 1.854850041988580043E-15 ) ) ;
#57395=ADVANCED_FACE ( 'NONE', ( #33453 ), #52218, .F. ) ;
#57427=FACE_OUTER_BOUND ( 'NONE', #60224, .T. ) ;
#57429=CIRCLE ( 'NONE', #11454, 15.14599999999999369 ) ;
#57430=CARTESIAN_POINT ( 'NONE',  ( 5.440000000000003055, -15.43999999999998529, 1.890854657883512518E-15 ) ) ;
#57536=DIRECTION ( 'NONE',  ( 1.000000000000000000, 0.000000000000000000, 0.000000000000000000 ) ) ;
#57725=CARTESIAN_POINT ( 'NONE',  ( 6.000000000000000888, -15.71999999999998820, 1.942289823447701485E-15 ) ) ;
#57963=CYLINDRICAL_SURFACE ( 'NONE', #39514, 12.49999999999999822 ) ;
#58328=ORIENTED_EDGE ( 'NONE', *, *, #53503, .F. ) ;
#58465=DIRECTION ( 'NONE',  ( 0.000000000000000000, 0.000000000000000000, -1.000000000000000000 ) ) ;
#58539=ORIENTED_EDGE ( 'NONE', *, *, #11776, .F. ) ;
#58595=CARTESIAN_POINT ( 'NONE',  ( -5.440000000000000391, 4.832908975360033023E-15, 0.000000000000000000 ) ) ;
#58653=DIRECTION ( 'NONE',  ( 0.000000000000000000, 0.000000000000000000, -1.000000000000000000 ) ) ;
#58696=AXIS2_PLACEMENT_3D ( 'NONE', #9002, #3973, #47534 ) ;
#58713=ADVANCED_FACE ( 'NONE', ( #47702, #43332 ), #14508, .T. ) ;
#58726=EDGE_CURVE ( 'NONE', #61046, #3794, #43023, .T. ) ;
#58730=CARTESIAN_POINT ( 'NONE',  ( 5.272380000000000067, 0.000000000000000000, 0.000000000000000000 ) ) ;
#58787=DIRECTION ( 'NONE',  ( 0.000000000000000000, 0.000000000000000000, 1.000000000000000000 ) ) ;
#58847=DIRECTION ( 'NONE',  ( 0.000000000000000000, 0.000000000000000000, 1.000000000000000000 ) ) ;
#58969=VECTOR ( 'NONE', #27362, 1000.000000000000000 ) ;
#59037=CARTESIAN_POINT ( 'NONE',  ( -5.331200000000000827, 0.000000000000000000, 0.000000000000000000 ) ) ;
#59152=CARTESIAN_POINT ( 'NONE',  ( -31.75000000000000000, 0.000000000000000000, 0.000000000000000000 ) ) ;
#59178=EDGE_LOOP ( 'NONE', ( #15132, #691, #3535, #3080, #48380 ) ) ;
#59219=AXIS2_PLACEMENT_3D ( 'NONE', #35137, #53582, #24796 ) ;
#59263=DIRECTION ( 'NONE',  ( -1.718001593797181987E-16, 1.000000000000000000, 0.000000000000000000 ) ) ;
#59344=DIRECTION ( 'NONE',  ( -1.000000000000000000, -0.000000000000000000, -0.000000000000000000 ) ) ;
#59367=AXIS2_PLACEMENT_3D ( 'NONE', #35872, #11756, #54941 ) ;
#59459=DIRECTION ( 'NONE',  ( -1.000000000000000000, -0.000000000000000000, -0.000000000000000000 ) ) ;
#59492=VERTEX_POINT ( 'NONE', #9327 ) ;
#59614=ORIENTED_EDGE ( 'NONE', *, *, #52897, .T. ) ;
#59669=CIRCLE ( 'NONE', #32688, 15.43999999999999240 ) ;
#59752=CARTESIAN_POINT ( 'NONE',  ( 5.719999999999998863, -15.99999999999998934, 1.959434878635764737E-15 ) ) ;
#59766=CARTESIAN_POINT ( 'NONE',  ( -5.331200000000000827, 1.887314203987178256E-15, -15.38218000000000174 ) ) ;
#59811=ORIENTED_EDGE ( 'NONE', *, *, #31695, .T. ) ;
#59841=STYLED_ITEM ( 'NONE', ( #33826 ), #24273 ) ;
#59939=AXIS2_PLACEMENT_3D ( 'NONE', #1752, #36233, #11810 ) ;
#59958=AXIS2_PLACEMENT_3D ( 'NONE', #51966, #27555, #42596 ) ;
#60148=DIRECTION ( 'NONE',  ( -1.000000000000000000, -0.000000000000000000, -0.000000000000000000 ) ) ;
#60165=EDGE_CURVE ( 'NONE', #3794, #40968, #46609, .T. ) ;
#60169=DIRECTION ( 'NONE',  ( -0.000000000000000000, 1.000000000000000000, 1.224646799147353207E-16 ) ) ;
#60206=DIRECTION ( 'NONE',  ( -1.000000000000000000, -0.000000000000000000, -0.000000000000000000 ) ) ;
#60224=EDGE_LOOP ( 'NONE', ( #15684, #38505 ) ) ;
#60308=AXIS2_PLACEMENT_3D ( 'NONE', #4434, #4136, #23889 ) ;
#60431=EDGE_CURVE ( 'NONE', #26687, #40968, #24639, .T. ) ;
#60443=CARTESIAN_POINT ( 'NONE',  ( -5.331200000000000827, 0.000000000000000000, 0.000000000000000000 ) ) ;
#60555=ADVANCED_FACE ( 'NONE', ( #6769 ), #47665, .T. ) ;
#60701=CARTESIAN_POINT ( 'NONE',  ( 5.272379999999998290, 0.000000000000000000, 12.55882000000000076 ) ) ;
#60727=DIRECTION ( 'NONE',  ( 0.000000000000000000, 0.000000000000000000, -1.000000000000000000 ) ) ;
#60745=EDGE_CURVE ( 'NONE', #536, #1749, #36683, .T. ) ;
#60799=AXIS2_PLACEMENT_3D ( 'NONE', #45525, #60206, #32342 ) ;
#60941=VECTOR ( 'NONE', #33195, 1000.000000000000000 ) ;
#60954=DIRECTION ( 'NONE',  ( -1.000000000000000000, -0.000000000000000000, -0.000000000000000000 ) ) ;
#61046=VERTEX_POINT ( 'NONE', #47121 ) ;
#61148=ADVANCED_FACE ( 'NONE', ( #2243 ), #3593, .T. ) ;
#61180=ORIENTED_EDGE ( 'NONE', *, *, #39693, .F. ) ;
#61196=AXIS2_PLACEMENT_3D ( 'NONE', #22327, #9143, #8212 ) ;
#61279=CARTESIAN_POINT ( 'NONE',  ( -5.440000000000003944, 15.43999999999999950, 0.000000000000000000 ) ) ;
#61285=CARTESIAN_POINT ( 'NONE',  ( -5.331200000000000827, 15.38218000000000174, 0.000000000000000000 ) ) ;
#61294=CYLINDRICAL_SURFACE ( 'NONE', #29062, 15.14599999999999369 ) ;
#61320=CIRCLE ( 'NONE', #7296, 12.49999999999999822 ) ;
#61337=ORIENTED_EDGE ( 'NONE', *, *, #23064, .T. ) ;
#61360=VECTOR ( 'NONE', #31169, 1000.000000000000000 ) ;
#61387=DIRECTION ( 'NONE',  ( 0.000000000000000000, 0.000000000000000000, 1.000000000000000000 ) ) ;
#61422=EDGE_CURVE ( 'NONE', #42948, #59492, #28224, .T. ) ;
#61475=AXIS2_PLACEMENT_3D ( 'NONE', #26410, #6971, #26106 ) ;
#61479=VERTEX_POINT ( 'NONE', #25072 ) ;
#61543=EDGE_CURVE ( 'NONE', #11235, #38956, #20704, .T. ) ;
#61581=CARTESIAN_POINT ( 'NONE',  ( -6.000000000000001776, 4.730042041638951881E-15, 0.000000000000000000 ) ) ;
#61592=AXIS2_PLACEMENT_3D ( 'NONE', #23905, #33015, #43036 ) ;
#61687=ORIENTED_EDGE ( 'NONE', *, *, #31973, .T. ) ;
#61804=AXIS2_PLACEMENT_3D ( 'NONE', #5504, #6414, #825 ) ;
#61884=VERTEX_POINT ( 'NONE', #51183 ) ;
#61911=DIRECTION ( 'NONE',  ( 0.000000000000000000, 1.000000000000000000, 0.000000000000000000 ) ) ;
#61961=DIRECTION ( 'NONE',  ( -1.836909530733573776E-16, 1.000000000000000000, 0.000000000000000000 ) ) ;
ENDSEC;
END-ISO-10303-21;
